ISO-10303-21;
HEADER;
/* Generated by software containing ST-Developer
 * from STEP Tools, Inc. (www.steptools.com) 
 */

FILE_DESCRIPTION(
/* description */ (''),
/* implementation_level */ '2;1');

FILE_NAME(
/* name */ 'Hex nut M3.step',
/* time_stamp */ '2026-11-10T05:40:20-08:00',
/* author */ (''),
/* organization */ (''),
/* preprocessor_version */ 'ST-DEVELOPER v20.2',
/* originating_system */ 'Autodesk Translation Framework v15.17.0.0',
/* authorisation */ '');

FILE_SCHEMA (('AUTOMOTIVE_DESIGN { 1 0 10303 214 3 1 1 }'));
ENDSEC;

DATA;
#10=MECHANICAL_DESIGN_GEOMETRIC_PRESENTATION_REPRESENTATION('',(#578),#18580);
#158=B_SPLINE_SURFACE_WITH_KNOTS('',3,3,((#17366,#17367,#17368,#17369,#17370,
#17371,#17372,#17373,#17374,#17375,#17376,#17377,#17378,#17379,#17380,#17381,
#17382,#17383,#17384,#17385,#17386,#17387,#17388,#17389,#17390,#17391,#17392,
#17393,#17394,#17395,#17396,#17397,#17398,#17399,#17400,#17401),(#17402,
#17403,#17404,#17405,#17406,#17407,#17408,#17409,#17410,#17411,#17412,#17413,
#17414,#17415,#17416,#17417,#17418,#17419,#17420,#17421,#17422,#17423,#17424,
#17425,#17426,#17427,#17428,#17429,#17430,#17431,#17432,#17433,#17434,#17435,
#17436,#17437),(#17438,#17439,#17440,#17441,#17442,#17443,#17444,#17445,
#17446,#17447,#17448,#17449,#17450,#17451,#17452,#17453,#17454,#17455,#17456,
#17457,#17458,#17459,#17460,#17461,#17462,#17463,#17464,#17465,#17466,#17467,
#17468,#17469,#17470,#17471,#17472,#17473),(#17474,#17475,#17476,#17477,
#17478,#17479,#17480,#17481,#17482,#17483,#17484,#17485,#17486,#17487,#17488,
#17489,#17490,#17491,#17492,#17493,#17494,#17495,#17496,#17497,#17498,#17499,
#17500,#17501,#17502,#17503,#17504,#17505,#17506,#17507,#17508,#17509)),
 .UNSPECIFIED.,.F.,.F.,.F.,(4,4),(4,1,1,1,1,1,1,1,1,1,1,1,1,1,1,1,1,1,1,
1,1,1,1,1,1,1,1,1,1,1,1,1,1,4),(0.,0.0321584099938622),(11.8553612635794,
12.830508595889,13.8056559281987,14.7808032605084,15.755950592818,16.7310979251277,
17.7062452574374,18.681392589747,19.6565399220567,20.6316872543664,21.606834586676,
22.5819819189857,23.5571292512954,24.532276583605,25.5074239159147,26.4825712482243,
27.457718580534,28.4328659128437,29.4080132451533,30.383160577463,31.3583079097727,
32.3334552420823,33.308602574392,34.2837499067017,35.2588972390113,36.234044571321,
37.2091919036307,38.1843392359403,39.15948656825,40.1346339005596,41.1097812328693,
42.084928565179,43.0600758974886,44.0352232297983),.UNSPECIFIED.);
#159=B_SPLINE_SURFACE_WITH_KNOTS('',3,3,((#17633,#17634,#17635,#17636,#17637,
#17638,#17639,#17640,#17641,#17642,#17643,#17644,#17645,#17646,#17647,#17648,
#17649,#17650,#17651,#17652,#17653,#17654,#17655,#17656,#17657,#17658,#17659,
#17660,#17661,#17662,#17663,#17664,#17665,#17666,#17667,#17668),(#17669,
#17670,#17671,#17672,#17673,#17674,#17675,#17676,#17677,#17678,#17679,#17680,
#17681,#17682,#17683,#17684,#17685,#17686,#17687,#17688,#17689,#17690,#17691,
#17692,#17693,#17694,#17695,#17696,#17697,#17698,#17699,#17700,#17701,#17702,
#17703,#17704),(#17705,#17706,#17707,#17708,#17709,#17710,#17711,#17712,
#17713,#17714,#17715,#17716,#17717,#17718,#17719,#17720,#17721,#17722,#17723,
#17724,#17725,#17726,#17727,#17728,#17729,#17730,#17731,#17732,#17733,#17734,
#17735,#17736,#17737,#17738,#17739,#17740),(#17741,#17742,#17743,#17744,
#17745,#17746,#17747,#17748,#17749,#17750,#17751,#17752,#17753,#17754,#17755,
#17756,#17757,#17758,#17759,#17760,#17761,#17762,#17763,#17764,#17765,#17766,
#17767,#17768,#17769,#17770,#17771,#17772,#17773,#17774,#17775,#17776)),
 .UNSPECIFIED.,.F.,.F.,.F.,(4,4),(4,1,1,1,1,1,1,1,1,1,1,1,1,1,1,1,1,1,1,
1,1,1,1,1,1,1,1,1,1,1,1,1,1,4),(0.,0.0321584099938622),(14.3984001269719,
15.3735474592815,16.3486947915912,17.3238421239009,18.2989894562105,19.2741367885202,
20.2492841208299,21.2244314531395,22.1995787854492,23.1747261177589,24.1498734500685,
25.1250207823782,26.1001681146879,27.0753154469975,28.0504627793072,29.0256101116168,
30.0007574439265,30.9759047762362,31.9510521085458,32.9261994408555,33.9013467731652,
34.8764941054748,35.8516414377845,36.8267887700942,37.8019361024038,38.7770834347135,
39.7522307670232,40.7273780993328,41.7025254316425,42.6776727639522,43.6528200962618,
44.6279674285715,45.6031147608811,46.5782620931908),.UNSPECIFIED.);
#501=B_SPLINE_CURVE_WITH_KNOTS('',3,(#17036,#17037,#17038,#17039,#17040,
#17041,#17042),.UNSPECIFIED.,.F.,.F.,(4,3,4),(-30.159289474462,-29.2544199692899,
-28.9853432330879),.UNSPECIFIED.);
#502=B_SPLINE_CURVE_WITH_KNOTS('',3,(#17048,#17049,#17050,#17051,#17052,
#17053,#17054,#17055,#17056,#17057,#17058,#17059,#17060,#17061,#17062,#17063,
#17064,#17065,#17066),.UNSPECIFIED.,.F.,.F.,(4,3,3,3,3,3,4),(26.4423043696954,
27.3041253046706,28.2792726369803,29.25441996929,30.2295673015996,31.2047146339093,
32.179861966219),.UNSPECIFIED.);
#503=B_SPLINE_CURVE_WITH_KNOTS('',3,(#17068,#17069,#17070,#17071,#17072,
#17073,#17074,#17075,#17076,#17077,#17078,#17079,#17080,#17081,#17082,#17083,
#17084,#17085,#17086,#17087,#17088,#17089),.UNSPECIFIED.,.F.,.F.,(4,3,3,
3,3,3,3,4),(-28.9853432330879,-28.2792726369803,-27.3041253046706,-26.3289779723609,
-25.3538306400513,-24.3786833077416,-23.403535975432,-22.7021579259084),
 .UNSPECIFIED.);
#504=B_SPLINE_CURVE_WITH_KNOTS('',3,(#17094,#17095,#17096,#17097,#17098,
#17099,#17100,#17101,#17102,#17103,#17104,#17105,#17106,#17107,#17108,#17109,
#17110,#17111,#17112,#17113,#17114,#17115,#17116,#17117,#17118),
 .UNSPECIFIED.,.F.,.F.,(4,3,3,3,3,3,3,3,4),(20.1591190625159,20.478093978503,
21.4532413108126,22.4283886431223,23.403535975432,24.3786833077416,25.3538306400513,
26.328977972361,26.4423043696954),.UNSPECIFIED.);
#505=B_SPLINE_CURVE_WITH_KNOTS('',3,(#17119,#17120,#17121,#17122,#17123,
#17124,#17125,#17126,#17127,#17128,#17129,#17130,#17131,#17132,#17133,#17134,
#17135,#17136,#17137,#17138,#17139,#17140,#17141,#17142,#17143),
 .UNSPECIFIED.,.F.,.F.,(4,3,3,3,3,3,3,3,4),(-22.7021579259084,-22.4283886431223,
-21.4532413108126,-20.478093978503,-19.5029466461933,-18.5277993138836,
-17.552651981574,-16.5775046492643,-16.4189726187288),.UNSPECIFIED.);
#506=B_SPLINE_CURVE_WITH_KNOTS('',3,(#17148,#17149,#17150,#17151,#17152,
#17153,#17154,#17155,#17156,#17157,#17158,#17159,#17160,#17161,#17162,#17163,
#17164,#17165,#17166,#17167,#17168,#17169),.UNSPECIFIED.,.F.,.F.,(4,3,3,
3,3,3,3,4),(13.8759337553363,14.627209984645,15.6023573169546,16.5775046492643,
17.552651981574,18.5277993138836,19.5029466461933,20.1591190625159),
 .UNSPECIFIED.);
#507=B_SPLINE_CURVE_WITH_KNOTS('',3,(#17170,#17171,#17172,#17173,#17174,
#17175,#17176,#17177,#17178,#17179,#17180,#17181,#17182,#17183,#17184,#17185,
#17186,#17187,#17188,#17189,#17190,#17191),.UNSPECIFIED.,.F.,.F.,(4,3,3,
3,3,3,3,4),(-16.4189726187288,-15.6023573169546,-14.627209984645,-13.6520626523353,
-12.6769153200256,-11.701767987716,-10.7266206554063,-10.1357873115492),
 .UNSPECIFIED.);
#508=B_SPLINE_CURVE_WITH_KNOTS('',3,(#17197,#17198,#17199,#17200,#17201,
#17202,#17203,#17204,#17205,#17206,#17207,#17208,#17209),.UNSPECIFIED.,
 .F.,.F.,(4,3,3,3,4),(-3.8526020043696,-2.92544199692899,-1.95029466461933,
-0.975147332309664,0.),.UNSPECIFIED.);
#509=B_SPLINE_CURVE_WITH_KNOTS('',3,(#17212,#17213,#17214,#17215,#17216,
#17217,#17218,#17219,#17220,#17221,#17222,#17223,#17224,#17225,#17226,#17227,
#17228,#17229,#17230),.UNSPECIFIED.,.F.,.F.,(4,3,3,3,3,3,4),(2.02057249175693,
2.925441996929,3.90058932923866,4.87573666154832,5.85088399385799,6.82603132616766,
7.59274844815668),.UNSPECIFIED.);
#510=B_SPLINE_CURVE_WITH_KNOTS('',3,(#17236,#17237,#17238,#17239,#17240,
#17241,#17242),.UNSPECIFIED.,.F.,.F.,(4,1,1,1,4),(40.8407044966673,41.1097812328693,
42.084928565179,43.0600758974886,44.0352232297983),.UNSPECIFIED.);
#511=B_SPLINE_CURVE_WITH_KNOTS('',3,(#17245,#17246,#17247,#17248,#17249,
#17250,#17251),.UNSPECIFIED.,.F.,.F.,(4,1,1,1,4),(40.8407044966673,41.7025254316425,
42.6776727639522,43.6528200962618,44.5576896014339),.UNSPECIFIED.);
#512=B_SPLINE_CURVE_WITH_KNOTS('',3,(#17256,#17257,#17258,#17259,#17260,
#17261,#17262,#17263,#17264,#17265),.UNSPECIFIED.,.F.,.F.,(4,1,1,1,1,1,
1,4),(34.5575191894877,35.2588972390113,36.234044571321,37.2091919036307,
38.1843392359403,39.15948656825,40.1346339005596,40.8407044966673),
 .UNSPECIFIED.);
#513=B_SPLINE_CURVE_WITH_KNOTS('',3,(#17266,#17267,#17268,#17269,#17270,
#17271,#17272,#17273,#17274,#17275,#17276),.UNSPECIFIED.,.F.,.F.,(4,1,1,
1,1,1,1,1,4),(34.5575191894877,34.8764941054748,35.8516414377845,36.8267887700942,
37.8019361024038,38.7770834347135,39.7522307670232,40.7273780993328,40.8407044966673),
 .UNSPECIFIED.);
#514=B_SPLINE_CURVE_WITH_KNOTS('',3,(#17281,#17282,#17283,#17284,#17285,
#17286,#17287,#17288,#17289,#17290,#17291),.UNSPECIFIED.,.F.,.F.,(4,1,1,
1,1,1,1,1,4),(28.2743338823081,28.4328659128437,29.4080132451533,30.383160577463,
31.3583079097727,32.3334552420823,33.308602574392,34.2837499067017,34.5575191894877),
 .UNSPECIFIED.);
#515=B_SPLINE_CURVE_WITH_KNOTS('',3,(#17292,#17293,#17294,#17295,#17296,
#17297,#17298,#17299,#17300,#17301),.UNSPECIFIED.,.F.,.F.,(4,1,1,1,1,1,
1,4),(28.2743338823081,29.0256101116168,30.0007574439265,30.9759047762362,
31.9510521085458,32.9261994408555,33.9013467731652,34.5575191894877),
 .UNSPECIFIED.);
#516=B_SPLINE_CURVE_WITH_KNOTS('',3,(#17306,#17307,#17308,#17309,#17310,
#17311,#17312,#17313,#17314,#17315),.UNSPECIFIED.,.F.,.F.,(4,1,1,1,1,1,
1,4),(21.9911485751285,22.5819819189857,23.5571292512954,24.532276583605,
25.5074239159147,26.4825712482243,27.457718580534,28.2743338823081),
 .UNSPECIFIED.);
#517=B_SPLINE_CURVE_WITH_KNOTS('',3,(#17316,#17317,#17318,#17319,#17320,
#17321,#17322,#17323,#17324,#17325,#17326),.UNSPECIFIED.,.F.,.F.,(4,1,1,
1,1,1,1,1,4),(21.9911485751285,22.1995787854492,23.1747261177589,24.1498734500685,
25.1250207823782,26.1001681146879,27.0753154469975,28.0504627793072,28.2743338823081),
 .UNSPECIFIED.);
#518=B_SPLINE_CURVE_WITH_KNOTS('',3,(#17332,#17333,#17334,#17335,#17336),
 .UNSPECIFIED.,.F.,.F.,(4,1,4),(14.3984001269719,15.3735474592815,15.7079632679489),
 .UNSPECIFIED.);
#519=B_SPLINE_CURVE_WITH_KNOTS('',3,(#17339,#17340,#17341,#17342,#17343),
 .UNSPECIFIED.,.F.,.F.,(4,1,4),(13.8759337553363,14.7808032605084,15.7079632679489),
 .UNSPECIFIED.);
#520=B_SPLINE_CURVE_WITH_KNOTS('',3,(#17345,#17346,#17347,#17348,#17349,
#17350,#17351,#17352,#17353,#17354,#17355),.UNSPECIFIED.,.F.,.F.,(4,1,1,
1,1,1,1,1,4),(15.7079632679489,15.755950592818,16.7310979251277,17.7062452574374,
18.681392589747,19.6565399220567,20.6316872543664,21.606834586676,21.9911485751285),
 .UNSPECIFIED.);
#521=B_SPLINE_CURVE_WITH_KNOTS('',3,(#17356,#17357,#17358,#17359,#17360,
#17361,#17362,#17363,#17364,#17365),.UNSPECIFIED.,.F.,.F.,(4,1,1,1,1,1,
1,4),(15.7079632679489,16.3486947915912,17.3238421239009,18.2989894562105,
19.2741367885202,20.2492841208299,21.2244314531395,21.9911485751285),
 .UNSPECIFIED.);
#522=B_SPLINE_CURVE_WITH_KNOTS('',3,(#17510,#17511,#17512,#17513,#17514,
#17515,#17516,#17517,#17518,#17519,#17520,#17521,#17522,#17523,#17524,#17525,
#17526,#17527,#17528,#17529,#17530,#17531,#17532,#17533,#17534,#17535,#17536,
#17537,#17538,#17539,#17540,#17541,#17542,#17543,#17544,#17545,#17546,#17547,
#17548,#17549,#17550,#17551,#17552,#17553,#17554,#17555,#17556,#17557,#17558),
 .UNSPECIFIED.,.F.,.F.,(4,3,3,3,3,3,3,3,3,3,3,3,3,3,3,3,4),(0.,0.0320333804888866,
0.0505515708593653,0.0603413132804416,0.0917900141854983,0.108096115778005,
0.122914675479851,0.145143248337739,0.168151513577436,0.177516949333476,
0.202471322707608,0.21794283081622,0.231200110368267,0.247503117401854,
0.263651632124391,0.277334442830003,0.286347380332244),.UNSPECIFIED.);
#523=B_SPLINE_CURVE_WITH_KNOTS('',3,(#17559,#17560,#17561,#17562,#17563,
#17564,#17565,#17566,#17567,#17568,#17569,#17570,#17571,#17572,#17573,#17574,
#17575,#17576,#17577,#17578,#17579,#17580,#17581,#17582,#17583,#17584,#17585,
#17586,#17587,#17588,#17589,#17590,#17591,#17592,#17593,#17594,#17595,#17596,
#17597,#17598,#17599,#17600,#17601,#17602,#17603,#17604,#17605,#17606,#17607),
 .UNSPECIFIED.,.F.,.F.,(4,3,3,3,3,3,3,3,3,3,3,3,3,3,3,3,4),(0.,0.0274305464075637,
0.0492901149097146,0.0591933555873536,0.0887250095166089,0.100015570674795,
0.108381796308415,0.130826479038955,0.152531076563578,0.162815893631175,
0.190691958353668,0.212372986031639,0.222945305605857,0.245534254906135,
0.257847836118801,0.274320152521146,0.28514280399515),.UNSPECIFIED.);
#524=B_SPLINE_CURVE_WITH_KNOTS('',3,(#17608,#17609,#17610,#17611,#17612,
#17613,#17614,#17615,#17616,#17617,#17618,#17619,#17620,#17621,#17622,#17623,
#17624,#17625,#17626,#17627,#17628,#17629,#17630,#17631,#17632),
 .UNSPECIFIED.,.F.,.F.,(4,3,3,3,3,3,3,3,4),(-10.1357873115492,-9.75147332309665,
-8.77632599078699,-7.80117865847732,-6.82603132616766,-5.85088399385799,
-4.87573666154833,-3.90058932923866,-3.8526020043696),.UNSPECIFIED.);
#525=B_SPLINE_CURVE_WITH_KNOTS('',3,(#17777,#17778,#17779,#17780,#17781,
#17782,#17783,#17784,#17785,#17786,#17787,#17788,#17789,#17790,#17791,#17792,
#17793,#17794,#17795,#17796,#17797,#17798,#17799,#17800,#17801,#17802,#17803,
#17804,#17805,#17806,#17807,#17808,#17809,#17810,#17811,#17812,#17813,#17814,
#17815,#17816,#17817,#17818,#17819,#17820,#17821,#17822,#17823,#17824,#17825),
 .UNSPECIFIED.,.F.,.F.,(4,3,3,3,3,3,3,3,3,3,3,3,3,3,3,3,4),(0.,0.0274305890506951,
0.0492901290331875,0.0591933603491513,0.0887250177779717,0.100015607166709,
0.108381835831352,0.13082647903896,0.152531071764912,0.162815892251191,
0.190691957318683,0.212372984486691,0.22294529735758,0.245534140364172,
0.257847701250626,0.274320152521159,0.285142803995162),.UNSPECIFIED.);
#526=B_SPLINE_CURVE_WITH_KNOTS('',3,(#17826,#17827,#17828,#17829,#17830,
#17831,#17832,#17833,#17834,#17835,#17836,#17837,#17838,#17839,#17840,#17841,
#17842,#17843,#17844,#17845,#17846,#17847,#17848,#17849,#17850),
 .UNSPECIFIED.,.F.,.F.,(4,3,3,3,3,3,3,3,4),(7.59274844815668,7.80117865847732,
8.77632599078698,9.75147332309665,10.7266206554063,11.701767987716,12.6769153200256,
13.6520626523353,13.8759337553363),.UNSPECIFIED.);
#527=B_SPLINE_CURVE_WITH_KNOTS('',3,(#17851,#17852,#17853,#17854,#17855,
#17856,#17857,#17858,#17859,#17860,#17861,#17862,#17863,#17864,#17865,#17866,
#17867,#17868,#17869,#17870,#17871,#17872,#17873,#17874,#17875,#17876,#17877,
#17878,#17879,#17880,#17881,#17882,#17883,#17884,#17885,#17886,#17887,#17888,
#17889,#17890,#17891,#17892,#17893,#17894,#17895,#17896,#17897,#17898,#17899),
 .UNSPECIFIED.,.F.,.F.,(4,3,3,3,3,3,3,3,3,3,3,3,3,3,3,3,4),(0.,0.0320334058164849,
0.0505515938322513,0.0603413311462071,0.0917900214840119,0.108096111687201,
0.122914678304232,0.145143248337743,0.168151527562726,0.177516955081398,
0.202471327018552,0.217942288122009,0.231200024743484,0.24750284136614,
0.263651600306541,0.277334442830014,0.286347380332252),.UNSPECIFIED.);
#560=SHAPE_REPRESENTATION_RELATIONSHIP('SRR','None',#18631,#569);
#569=ADVANCED_BREP_SHAPE_REPRESENTATION('',(#587),#18577);
#578=STYLED_ITEM('',(#18687),#587);
#587=MANIFOLD_SOLID_BREP('Body1',#6550);
#635=FACE_BOUND('',#1545,.T.);
#636=FACE_BOUND('',#1554,.T.);
#774=PLANE('',#7047);
#775=PLANE('',#7049);
#776=PLANE('',#7050);
#777=PLANE('',#7051);
#778=PLANE('',#7052);
#779=PLANE('',#7053);
#780=PLANE('',#7054);
#781=PLANE('',#7055);
#1110=FACE_OUTER_BOUND('',#1531,.T.);
#1111=FACE_OUTER_BOUND('',#1532,.T.);
#1112=FACE_OUTER_BOUND('',#1533,.T.);
#1113=FACE_OUTER_BOUND('',#1534,.T.);
#1114=FACE_OUTER_BOUND('',#1535,.T.);
#1115=FACE_OUTER_BOUND('',#1536,.T.);
#1116=FACE_OUTER_BOUND('',#1537,.T.);
#1117=FACE_OUTER_BOUND('',#1538,.T.);
#1118=FACE_OUTER_BOUND('',#1539,.T.);
#1119=FACE_OUTER_BOUND('',#1540,.T.);
#1120=FACE_OUTER_BOUND('',#1541,.T.);
#1121=FACE_OUTER_BOUND('',#1542,.T.);
#1122=FACE_OUTER_BOUND('',#1543,.T.);
#1123=FACE_OUTER_BOUND('',#1544,.T.);
#1124=FACE_OUTER_BOUND('',#1546,.T.);
#1125=FACE_OUTER_BOUND('',#1547,.T.);
#1126=FACE_OUTER_BOUND('',#1548,.T.);
#1127=FACE_OUTER_BOUND('',#1549,.T.);
#1128=FACE_OUTER_BOUND('',#1550,.T.);
#1129=FACE_OUTER_BOUND('',#1551,.T.);
#1130=FACE_OUTER_BOUND('',#1552,.T.);
#1131=FACE_OUTER_BOUND('',#1553,.T.);
#1531=EDGE_LOOP('',(#5762,#5763,#5764));
#1532=EDGE_LOOP('',(#5765,#5766,#5767,#5768,#5769));
#1533=EDGE_LOOP('',(#5770,#5771,#5772,#5773));
#1534=EDGE_LOOP('',(#5774,#5775,#5776,#5777));
#1535=EDGE_LOOP('',(#5778,#5779,#5780,#5781));
#1536=EDGE_LOOP('',(#5782,#5783,#5784,#5785));
#1537=EDGE_LOOP('',(#5786,#5787,#5788,#5789));
#1538=EDGE_LOOP('',(#5790,#5791,#5792,#5793));
#1539=EDGE_LOOP('',(#5794,#5795,#5796,#5797));
#1540=EDGE_LOOP('',(#5798,#5799,#5800,#5801));
#1541=EDGE_LOOP('',(#5802,#5803,#5804,#5805));
#1542=EDGE_LOOP('',(#5806,#5807,#5808,#5809,#5810,#5811,#5812,#5813,#5814,
#5815,#5816,#5817,#5818,#5819));
#1543=EDGE_LOOP('',(#5820,#5821,#5822,#5823,#5824,#5825,#5826,#5827,#5828,
#5829,#5830,#5831,#5832));
#1544=EDGE_LOOP('',(#5833,#5834,#5835,#5836,#5837,#5838));
#1545=EDGE_LOOP('',(#5839,#5840,#5841,#5842));
#1546=EDGE_LOOP('',(#5843,#5844,#5845,#5846));
#1547=EDGE_LOOP('',(#5847,#5848,#5849,#5850));
#1548=EDGE_LOOP('',(#5851,#5852,#5853,#5854));
#1549=EDGE_LOOP('',(#5855,#5856,#5857,#5858));
#1550=EDGE_LOOP('',(#5859,#5860,#5861,#5862));
#1551=EDGE_LOOP('',(#5863,#5864,#5865,#5866));
#1552=EDGE_LOOP('',(#5867,#5868,#5869,#5870));
#1553=EDGE_LOOP('',(#5871,#5872,#5873,#5874,#5875,#5876));
#1554=EDGE_LOOP('',(#5877,#5878,#5879,#5880,#5881));
#1970=LINE('',#17033,#2377);
#1971=LINE('',#17046,#2378);
#1972=LINE('',#17093,#2379);
#1973=LINE('',#17147,#2380);
#1974=LINE('',#17195,#2381);
#1975=LINE('',#17234,#2382);
#1976=LINE('',#17255,#2383);
#1977=LINE('',#17280,#2384);
#1978=LINE('',#17305,#2385);
#1979=LINE('',#17330,#2386);
#1980=LINE('',#17903,#2387);
#1981=LINE('',#17905,#2388);
#1982=LINE('',#17907,#2389);
#1983=LINE('',#17909,#2390);
#1984=LINE('',#17911,#2391);
#1985=LINE('',#17912,#2392);
#1986=LINE('',#17917,#2393);
#1987=LINE('',#17918,#2394);
#1988=LINE('',#17919,#2395);
#1989=LINE('',#17922,#2396);
#1990=LINE('',#17923,#2397);
#1991=LINE('',#17926,#2398);
#1992=LINE('',#17927,#2399);
#1993=LINE('',#17930,#2400);
#1994=LINE('',#17931,#2401);
#1995=LINE('',#17934,#2402);
#1996=LINE('',#17935,#2403);
#1997=LINE('',#17937,#2404);
#2377=VECTOR('',#8253,0.15);
#2378=VECTOR('',#8258,0.15);
#2379=VECTOR('',#8263,0.15);
#2380=VECTOR('',#8266,0.15);
#2381=VECTOR('',#8269,0.15);
#2382=VECTOR('',#8274,0.1543);
#2383=VECTOR('',#8279,0.1543);
#2384=VECTOR('',#8282,0.1543);
#2385=VECTOR('',#8285,0.1543);
#2386=VECTOR('',#8288,0.1543);
#2387=VECTOR('',#8295,1.);
#2388=VECTOR('',#8296,1.);
#2389=VECTOR('',#8297,1.);
#2390=VECTOR('',#8298,1.);
#2391=VECTOR('',#8299,1.);
#2392=VECTOR('',#8300,1.);
#2393=VECTOR('',#8305,1.);
#2394=VECTOR('',#8306,1.);
#2395=VECTOR('',#8307,1.);
#2396=VECTOR('',#8310,1.);
#2397=VECTOR('',#8311,1.);
#2398=VECTOR('',#8314,1.);
#2399=VECTOR('',#8315,1.);
#2400=VECTOR('',#8318,1.);
#2401=VECTOR('',#8319,1.);
#2402=VECTOR('',#8322,1.);
#2403=VECTOR('',#8323,1.);
#2404=VECTOR('',#8326,1.);
#2544=CIRCLE('',#7032,0.12645);
#2545=CIRCLE('',#7034,0.12645);
#2546=CIRCLE('',#7038,0.12645);
#2547=CIRCLE('',#7040,0.1543);
#2548=CIRCLE('',#7045,0.1543);
#3105=VERTEX_POINT('',#17031);
#3106=VERTEX_POINT('',#17032);
#3107=VERTEX_POINT('',#17034);
#3108=VERTEX_POINT('',#17044);
#3109=VERTEX_POINT('',#17045);
#3110=VERTEX_POINT('',#17047);
#3111=VERTEX_POINT('',#17091);
#3112=VERTEX_POINT('',#17092);
#3113=VERTEX_POINT('',#17145);
#3114=VERTEX_POINT('',#17146);
#3115=VERTEX_POINT('',#17193);
#3116=VERTEX_POINT('',#17194);
#3117=VERTEX_POINT('',#17196);
#3118=VERTEX_POINT('',#17210);
#3119=VERTEX_POINT('',#17232);
#3120=VERTEX_POINT('',#17233);
#3121=VERTEX_POINT('',#17235);
#3122=VERTEX_POINT('',#17243);
#3123=VERTEX_POINT('',#17253);
#3124=VERTEX_POINT('',#17254);
#3125=VERTEX_POINT('',#17278);
#3126=VERTEX_POINT('',#17279);
#3127=VERTEX_POINT('',#17303);
#3128=VERTEX_POINT('',#17304);
#3129=VERTEX_POINT('',#17328);
#3130=VERTEX_POINT('',#17329);
#3131=VERTEX_POINT('',#17331);
#3132=VERTEX_POINT('',#17337);
#3133=VERTEX_POINT('',#17901);
#3134=VERTEX_POINT('',#17902);
#3135=VERTEX_POINT('',#17904);
#3136=VERTEX_POINT('',#17906);
#3137=VERTEX_POINT('',#17908);
#3138=VERTEX_POINT('',#17910);
#3139=VERTEX_POINT('',#17915);
#3140=VERTEX_POINT('',#17916);
#3141=VERTEX_POINT('',#17921);
#3142=VERTEX_POINT('',#17925);
#3143=VERTEX_POINT('',#17929);
#3144=VERTEX_POINT('',#17933);
#4004=EDGE_CURVE('',#3105,#3106,#1970,.T.);
#4005=EDGE_CURVE('',#3107,#3106,#2544,.F.);
#4006=EDGE_CURVE('',#3107,#3105,#501,.T.);
#4007=EDGE_CURVE('',#3108,#3109,#1971,.T.);
#4008=EDGE_CURVE('',#3109,#3110,#502,.T.);
#4009=EDGE_CURVE('',#3106,#3110,#2545,.F.);
#4010=EDGE_CURVE('',#3105,#3108,#503,.T.);
#4011=EDGE_CURVE('',#3111,#3112,#1972,.T.);
#4012=EDGE_CURVE('',#3112,#3109,#504,.T.);
#4013=EDGE_CURVE('',#3108,#3111,#505,.T.);
#4014=EDGE_CURVE('',#3113,#3114,#1973,.T.);
#4015=EDGE_CURVE('',#3114,#3112,#506,.T.);
#4016=EDGE_CURVE('',#3111,#3113,#507,.T.);
#4017=EDGE_CURVE('',#3115,#3116,#1974,.T.);
#4018=EDGE_CURVE('',#3115,#3117,#508,.T.);
#4019=EDGE_CURVE('',#3118,#3117,#2546,.T.);
#4020=EDGE_CURVE('',#3118,#3116,#509,.T.);
#4021=EDGE_CURVE('',#3119,#3120,#1975,.T.);
#4022=EDGE_CURVE('',#3120,#3121,#510,.T.);
#4023=EDGE_CURVE('',#3122,#3121,#2547,.T.);
#4024=EDGE_CURVE('',#3119,#3122,#511,.T.);
#4025=EDGE_CURVE('',#3123,#3124,#1976,.T.);
#4026=EDGE_CURVE('',#3124,#3120,#512,.T.);
#4027=EDGE_CURVE('',#3123,#3119,#513,.T.);
#4028=EDGE_CURVE('',#3125,#3126,#1977,.T.);
#4029=EDGE_CURVE('',#3126,#3124,#514,.T.);
#4030=EDGE_CURVE('',#3125,#3123,#515,.T.);
#4031=EDGE_CURVE('',#3127,#3128,#1978,.T.);
#4032=EDGE_CURVE('',#3128,#3126,#516,.T.);
#4033=EDGE_CURVE('',#3127,#3125,#517,.T.);
#4034=EDGE_CURVE('',#3129,#3130,#1979,.T.);
#4035=EDGE_CURVE('',#3131,#3129,#518,.T.);
#4036=EDGE_CURVE('',#3132,#3131,#2548,.T.);
#4037=EDGE_CURVE('',#3132,#3130,#519,.T.);
#4038=EDGE_CURVE('',#3130,#3128,#520,.T.);
#4039=EDGE_CURVE('',#3129,#3127,#521,.T.);
#4040=EDGE_CURVE('',#3121,#3107,#522,.T.);
#4041=EDGE_CURVE('',#3117,#3132,#523,.T.);
#4042=EDGE_CURVE('',#3113,#3115,#524,.T.);
#4043=EDGE_CURVE('',#3110,#3122,#525,.T.);
#4044=EDGE_CURVE('',#3116,#3114,#526,.T.);
#4045=EDGE_CURVE('',#3131,#3118,#527,.T.);
#4046=EDGE_CURVE('',#3133,#3134,#1980,.T.);
#4047=EDGE_CURVE('',#3134,#3135,#1981,.T.);
#4048=EDGE_CURVE('',#3135,#3136,#1982,.T.);
#4049=EDGE_CURVE('',#3136,#3137,#1983,.T.);
#4050=EDGE_CURVE('',#3137,#3138,#1984,.T.);
#4051=EDGE_CURVE('',#3138,#3133,#1985,.T.);
#4052=EDGE_CURVE('',#3139,#3140,#1986,.T.);
#4053=EDGE_CURVE('',#3140,#3133,#1987,.T.);
#4054=EDGE_CURVE('',#3139,#3138,#1988,.T.);
#4055=EDGE_CURVE('',#3141,#3139,#1989,.T.);
#4056=EDGE_CURVE('',#3141,#3137,#1990,.T.);
#4057=EDGE_CURVE('',#3142,#3141,#1991,.T.);
#4058=EDGE_CURVE('',#3142,#3136,#1992,.T.);
#4059=EDGE_CURVE('',#3143,#3142,#1993,.T.);
#4060=EDGE_CURVE('',#3143,#3135,#1994,.T.);
#4061=EDGE_CURVE('',#3144,#3143,#1995,.T.);
#4062=EDGE_CURVE('',#3144,#3134,#1996,.T.);
#4063=EDGE_CURVE('',#3140,#3144,#1997,.T.);
#5762=ORIENTED_EDGE('',*,*,#4004,.T.);
#5763=ORIENTED_EDGE('',*,*,#4005,.F.);
#5764=ORIENTED_EDGE('',*,*,#4006,.T.);
#5765=ORIENTED_EDGE('',*,*,#4007,.T.);
#5766=ORIENTED_EDGE('',*,*,#4008,.T.);
#5767=ORIENTED_EDGE('',*,*,#4009,.F.);
#5768=ORIENTED_EDGE('',*,*,#4004,.F.);
#5769=ORIENTED_EDGE('',*,*,#4010,.T.);
#5770=ORIENTED_EDGE('',*,*,#4011,.T.);
#5771=ORIENTED_EDGE('',*,*,#4012,.T.);
#5772=ORIENTED_EDGE('',*,*,#4007,.F.);
#5773=ORIENTED_EDGE('',*,*,#4013,.T.);
#5774=ORIENTED_EDGE('',*,*,#4014,.T.);
#5775=ORIENTED_EDGE('',*,*,#4015,.T.);
#5776=ORIENTED_EDGE('',*,*,#4011,.F.);
#5777=ORIENTED_EDGE('',*,*,#4016,.T.);
#5778=ORIENTED_EDGE('',*,*,#4017,.F.);
#5779=ORIENTED_EDGE('',*,*,#4018,.T.);
#5780=ORIENTED_EDGE('',*,*,#4019,.F.);
#5781=ORIENTED_EDGE('',*,*,#4020,.T.);
#5782=ORIENTED_EDGE('',*,*,#4021,.T.);
#5783=ORIENTED_EDGE('',*,*,#4022,.T.);
#5784=ORIENTED_EDGE('',*,*,#4023,.F.);
#5785=ORIENTED_EDGE('',*,*,#4024,.F.);
#5786=ORIENTED_EDGE('',*,*,#4025,.T.);
#5787=ORIENTED_EDGE('',*,*,#4026,.T.);
#5788=ORIENTED_EDGE('',*,*,#4021,.F.);
#5789=ORIENTED_EDGE('',*,*,#4027,.F.);
#5790=ORIENTED_EDGE('',*,*,#4028,.T.);
#5791=ORIENTED_EDGE('',*,*,#4029,.T.);
#5792=ORIENTED_EDGE('',*,*,#4025,.F.);
#5793=ORIENTED_EDGE('',*,*,#4030,.F.);
#5794=ORIENTED_EDGE('',*,*,#4031,.T.);
#5795=ORIENTED_EDGE('',*,*,#4032,.T.);
#5796=ORIENTED_EDGE('',*,*,#4028,.F.);
#5797=ORIENTED_EDGE('',*,*,#4033,.F.);
#5798=ORIENTED_EDGE('',*,*,#4034,.F.);
#5799=ORIENTED_EDGE('',*,*,#4035,.F.);
#5800=ORIENTED_EDGE('',*,*,#4036,.F.);
#5801=ORIENTED_EDGE('',*,*,#4037,.T.);
#5802=ORIENTED_EDGE('',*,*,#4034,.T.);
#5803=ORIENTED_EDGE('',*,*,#4038,.T.);
#5804=ORIENTED_EDGE('',*,*,#4031,.F.);
#5805=ORIENTED_EDGE('',*,*,#4039,.F.);
#5806=ORIENTED_EDGE('',*,*,#4040,.F.);
#5807=ORIENTED_EDGE('',*,*,#4022,.F.);
#5808=ORIENTED_EDGE('',*,*,#4026,.F.);
#5809=ORIENTED_EDGE('',*,*,#4029,.F.);
#5810=ORIENTED_EDGE('',*,*,#4032,.F.);
#5811=ORIENTED_EDGE('',*,*,#4038,.F.);
#5812=ORIENTED_EDGE('',*,*,#4037,.F.);
#5813=ORIENTED_EDGE('',*,*,#4041,.F.);
#5814=ORIENTED_EDGE('',*,*,#4018,.F.);
#5815=ORIENTED_EDGE('',*,*,#4042,.F.);
#5816=ORIENTED_EDGE('',*,*,#4016,.F.);
#5817=ORIENTED_EDGE('',*,*,#4013,.F.);
#5818=ORIENTED_EDGE('',*,*,#4010,.F.);
#5819=ORIENTED_EDGE('',*,*,#4006,.F.);
#5820=ORIENTED_EDGE('',*,*,#4043,.F.);
#5821=ORIENTED_EDGE('',*,*,#4008,.F.);
#5822=ORIENTED_EDGE('',*,*,#4012,.F.);
#5823=ORIENTED_EDGE('',*,*,#4015,.F.);
#5824=ORIENTED_EDGE('',*,*,#4044,.F.);
#5825=ORIENTED_EDGE('',*,*,#4020,.F.);
#5826=ORIENTED_EDGE('',*,*,#4045,.F.);
#5827=ORIENTED_EDGE('',*,*,#4035,.T.);
#5828=ORIENTED_EDGE('',*,*,#4039,.T.);
#5829=ORIENTED_EDGE('',*,*,#4033,.T.);
#5830=ORIENTED_EDGE('',*,*,#4030,.T.);
#5831=ORIENTED_EDGE('',*,*,#4027,.T.);
#5832=ORIENTED_EDGE('',*,*,#4024,.T.);
#5833=ORIENTED_EDGE('',*,*,#4046,.T.);
#5834=ORIENTED_EDGE('',*,*,#4047,.T.);
#5835=ORIENTED_EDGE('',*,*,#4048,.T.);
#5836=ORIENTED_EDGE('',*,*,#4049,.T.);
#5837=ORIENTED_EDGE('',*,*,#4050,.T.);
#5838=ORIENTED_EDGE('',*,*,#4051,.T.);
#5839=ORIENTED_EDGE('',*,*,#4041,.T.);
#5840=ORIENTED_EDGE('',*,*,#4036,.T.);
#5841=ORIENTED_EDGE('',*,*,#4045,.T.);
#5842=ORIENTED_EDGE('',*,*,#4019,.T.);
#5843=ORIENTED_EDGE('',*,*,#4017,.T.);
#5844=ORIENTED_EDGE('',*,*,#4044,.T.);
#5845=ORIENTED_EDGE('',*,*,#4014,.F.);
#5846=ORIENTED_EDGE('',*,*,#4042,.T.);
#5847=ORIENTED_EDGE('',*,*,#4052,.T.);
#5848=ORIENTED_EDGE('',*,*,#4053,.T.);
#5849=ORIENTED_EDGE('',*,*,#4051,.F.);
#5850=ORIENTED_EDGE('',*,*,#4054,.F.);
#5851=ORIENTED_EDGE('',*,*,#4055,.T.);
#5852=ORIENTED_EDGE('',*,*,#4054,.T.);
#5853=ORIENTED_EDGE('',*,*,#4050,.F.);
#5854=ORIENTED_EDGE('',*,*,#4056,.F.);
#5855=ORIENTED_EDGE('',*,*,#4057,.T.);
#5856=ORIENTED_EDGE('',*,*,#4056,.T.);
#5857=ORIENTED_EDGE('',*,*,#4049,.F.);
#5858=ORIENTED_EDGE('',*,*,#4058,.F.);
#5859=ORIENTED_EDGE('',*,*,#4059,.T.);
#5860=ORIENTED_EDGE('',*,*,#4058,.T.);
#5861=ORIENTED_EDGE('',*,*,#4048,.F.);
#5862=ORIENTED_EDGE('',*,*,#4060,.F.);
#5863=ORIENTED_EDGE('',*,*,#4061,.T.);
#5864=ORIENTED_EDGE('',*,*,#4060,.T.);
#5865=ORIENTED_EDGE('',*,*,#4047,.F.);
#5866=ORIENTED_EDGE('',*,*,#4062,.F.);
#5867=ORIENTED_EDGE('',*,*,#4063,.T.);
#5868=ORIENTED_EDGE('',*,*,#4062,.T.);
#5869=ORIENTED_EDGE('',*,*,#4046,.F.);
#5870=ORIENTED_EDGE('',*,*,#4053,.F.);
#5871=ORIENTED_EDGE('',*,*,#4063,.F.);
#5872=ORIENTED_EDGE('',*,*,#4052,.F.);
#5873=ORIENTED_EDGE('',*,*,#4055,.F.);
#5874=ORIENTED_EDGE('',*,*,#4057,.F.);
#5875=ORIENTED_EDGE('',*,*,#4059,.F.);
#5876=ORIENTED_EDGE('',*,*,#4061,.F.);
#5877=ORIENTED_EDGE('',*,*,#4040,.T.);
#5878=ORIENTED_EDGE('',*,*,#4005,.T.);
#5879=ORIENTED_EDGE('',*,*,#4009,.T.);
#5880=ORIENTED_EDGE('',*,*,#4043,.T.);
#5881=ORIENTED_EDGE('',*,*,#4023,.T.);
#6142=CYLINDRICAL_SURFACE('',#7031,0.12645);
#6143=CYLINDRICAL_SURFACE('',#7033,0.12645);
#6144=CYLINDRICAL_SURFACE('',#7035,0.12645);
#6145=CYLINDRICAL_SURFACE('',#7036,0.12645);
#6146=CYLINDRICAL_SURFACE('',#7037,0.12645);
#6147=CYLINDRICAL_SURFACE('',#7039,0.1543);
#6148=CYLINDRICAL_SURFACE('',#7041,0.1543);
#6149=CYLINDRICAL_SURFACE('',#7042,0.1543);
#6150=CYLINDRICAL_SURFACE('',#7043,0.1543);
#6151=CYLINDRICAL_SURFACE('',#7044,0.1543);
#6152=CYLINDRICAL_SURFACE('',#7046,0.1543);
#6153=CYLINDRICAL_SURFACE('',#7048,0.12645);
#6482=ADVANCED_FACE('',(#1110),#6142,.F.);
#6483=ADVANCED_FACE('',(#1111),#6143,.F.);
#6484=ADVANCED_FACE('',(#1112),#6144,.F.);
#6485=ADVANCED_FACE('',(#1113),#6145,.F.);
#6486=ADVANCED_FACE('',(#1114),#6146,.F.);
#6487=ADVANCED_FACE('',(#1115),#6147,.F.);
#6488=ADVANCED_FACE('',(#1116),#6148,.F.);
#6489=ADVANCED_FACE('',(#1117),#6149,.F.);
#6490=ADVANCED_FACE('',(#1118),#6150,.F.);
#6491=ADVANCED_FACE('',(#1119),#6151,.F.);
#6492=ADVANCED_FACE('',(#1120),#6152,.F.);
#6493=ADVANCED_FACE('',(#1121),#158,.F.);
#6494=ADVANCED_FACE('',(#1122),#159,.F.);
#6495=ADVANCED_FACE('',(#1123,#635),#774,.T.);
#6496=ADVANCED_FACE('',(#1124),#6153,.F.);
#6497=ADVANCED_FACE('',(#1125),#775,.T.);
#6498=ADVANCED_FACE('',(#1126),#776,.T.);
#6499=ADVANCED_FACE('',(#1127),#777,.T.);
#6500=ADVANCED_FACE('',(#1128),#778,.T.);
#6501=ADVANCED_FACE('',(#1129),#779,.T.);
#6502=ADVANCED_FACE('',(#1130),#780,.T.);
#6503=ADVANCED_FACE('',(#1131,#636),#781,.F.);
#6550=CLOSED_SHELL('',(#6482,#6483,#6484,#6485,#6486,#6487,#6488,#6489,
#6490,#6491,#6492,#6493,#6494,#6495,#6496,#6497,#6498,#6499,#6500,#6501,
#6502,#6503));
#7030=AXIS2_PLACEMENT_3D('',#17029,#8249,#8250);
#7031=AXIS2_PLACEMENT_3D('',#17030,#8251,#8252);
#7032=AXIS2_PLACEMENT_3D('',#17035,#8254,#8255);
#7033=AXIS2_PLACEMENT_3D('',#17043,#8256,#8257);
#7034=AXIS2_PLACEMENT_3D('',#17067,#8259,#8260);
#7035=AXIS2_PLACEMENT_3D('',#17090,#8261,#8262);
#7036=AXIS2_PLACEMENT_3D('',#17144,#8264,#8265);
#7037=AXIS2_PLACEMENT_3D('',#17192,#8267,#8268);
#7038=AXIS2_PLACEMENT_3D('',#17211,#8270,#8271);
#7039=AXIS2_PLACEMENT_3D('',#17231,#8272,#8273);
#7040=AXIS2_PLACEMENT_3D('',#17244,#8275,#8276);
#7041=AXIS2_PLACEMENT_3D('',#17252,#8277,#8278);
#7042=AXIS2_PLACEMENT_3D('',#17277,#8280,#8281);
#7043=AXIS2_PLACEMENT_3D('',#17302,#8283,#8284);
#7044=AXIS2_PLACEMENT_3D('',#17327,#8286,#8287);
#7045=AXIS2_PLACEMENT_3D('',#17338,#8289,#8290);
#7046=AXIS2_PLACEMENT_3D('',#17344,#8291,#8292);
#7047=AXIS2_PLACEMENT_3D('',#17900,#8293,#8294);
#7048=AXIS2_PLACEMENT_3D('',#17913,#8301,#8302);
#7049=AXIS2_PLACEMENT_3D('',#17914,#8303,#8304);
#7050=AXIS2_PLACEMENT_3D('',#17920,#8308,#8309);
#7051=AXIS2_PLACEMENT_3D('',#17924,#8312,#8313);
#7052=AXIS2_PLACEMENT_3D('',#17928,#8316,#8317);
#7053=AXIS2_PLACEMENT_3D('',#17932,#8320,#8321);
#7054=AXIS2_PLACEMENT_3D('',#17936,#8324,#8325);
#7055=AXIS2_PLACEMENT_3D('',#17938,#8327,#8328);
#8249=DIRECTION('axis',(0.,0.,1.));
#8250=DIRECTION('refdir',(1.,0.,0.));
#8251=DIRECTION('center_axis',(0.,0.,-1.));
#8252=DIRECTION('ref_axis',(1.,0.,0.));
#8253=DIRECTION('',(0.,0.,-1.));
#8254=DIRECTION('center_axis',(0.,0.,-1.));
#8255=DIRECTION('ref_axis',(1.,0.,0.));
#8256=DIRECTION('center_axis',(0.,0.,-1.));
#8257=DIRECTION('ref_axis',(1.,0.,0.));
#8258=DIRECTION('',(0.,0.,-1.));
#8259=DIRECTION('center_axis',(0.,0.,-1.));
#8260=DIRECTION('ref_axis',(1.,0.,0.));
#8261=DIRECTION('center_axis',(0.,0.,-1.));
#8262=DIRECTION('ref_axis',(1.,0.,0.));
#8263=DIRECTION('',(0.,0.,-1.));
#8264=DIRECTION('center_axis',(0.,0.,-1.));
#8265=DIRECTION('ref_axis',(1.,0.,0.));
#8266=DIRECTION('',(0.,0.,-1.));
#8267=DIRECTION('center_axis',(0.,0.,-1.));
#8268=DIRECTION('ref_axis',(0.937385399639056,-0.348293859468591,0.));
#8269=DIRECTION('',(0.,0.,-1.));
#8270=DIRECTION('center_axis',(0.,0.,-1.));
#8271=DIRECTION('ref_axis',(1.,0.,0.));
#8272=DIRECTION('center_axis',(0.,0.,-1.));
#8273=DIRECTION('ref_axis',(0.28361887368566,0.958937085782627,0.));
#8274=DIRECTION('',(1.22464679914735E-16,8.07419868282478E-31,-1.));
#8275=DIRECTION('center_axis',(0.,0.,1.));
#8276=DIRECTION('ref_axis',(1.,6.71554824363804E-15,0.));
#8277=DIRECTION('center_axis',(0.,0.,-1.));
#8278=DIRECTION('ref_axis',(1.,6.71554824363804E-15,0.));
#8279=DIRECTION('',(1.22464679914735E-16,8.07419868282478E-31,-1.));
#8280=DIRECTION('center_axis',(0.,0.,-1.));
#8281=DIRECTION('ref_axis',(1.,6.71554824363804E-15,0.));
#8282=DIRECTION('',(1.22464679914735E-16,8.07419868282478E-31,-1.));
#8283=DIRECTION('center_axis',(0.,0.,-1.));
#8284=DIRECTION('ref_axis',(1.,6.71554824363804E-15,0.));
#8285=DIRECTION('',(1.22464679914735E-16,8.07419868282478E-31,-1.));
#8286=DIRECTION('center_axis',(0.,0.,-1.));
#8287=DIRECTION('ref_axis',(-0.60895050335979,-0.793208222636313,0.));
#8288=DIRECTION('',(1.22464679914735E-16,8.07419868282478E-31,-1.));
#8289=DIRECTION('center_axis',(0.,0.,-1.));
#8290=DIRECTION('ref_axis',(1.,6.71554824363804E-15,0.));
#8291=DIRECTION('center_axis',(0.,0.,-1.));
#8292=DIRECTION('ref_axis',(1.,6.71554824363804E-15,0.));
#8293=DIRECTION('center_axis',(0.,0.,1.));
#8294=DIRECTION('ref_axis',(1.,0.,0.));
#8295=DIRECTION('',(0.5,0.866025403784439,0.));
#8296=DIRECTION('',(-0.5,0.866025403784439,0.));
#8297=DIRECTION('',(-1.,0.,0.));
#8298=DIRECTION('',(-0.5,-0.866025403784439,0.));
#8299=DIRECTION('',(0.5,-0.866025403784439,0.));
#8300=DIRECTION('',(1.,-3.49629579342466E-16,0.));
#8301=DIRECTION('center_axis',(0.,0.,-1.));
#8302=DIRECTION('ref_axis',(1.,0.,0.));
#8303=DIRECTION('center_axis',(-3.49629579342466E-16,-1.,0.));
#8304=DIRECTION('ref_axis',(1.,-3.49629579342466E-16,0.));
#8305=DIRECTION('',(1.,-3.49629579342466E-16,0.));
#8306=DIRECTION('',(0.,0.,1.));
#8307=DIRECTION('',(0.,0.,1.));
#8308=DIRECTION('center_axis',(-0.866025403784439,-0.5,0.));
#8309=DIRECTION('ref_axis',(0.5,-0.866025403784439,0.));
#8310=DIRECTION('',(0.5,-0.866025403784439,0.));
#8311=DIRECTION('',(0.,0.,1.));
#8312=DIRECTION('center_axis',(-0.866025403784439,0.5,0.));
#8313=DIRECTION('ref_axis',(-0.5,-0.866025403784439,0.));
#8314=DIRECTION('',(-0.5,-0.866025403784439,0.));
#8315=DIRECTION('',(0.,0.,1.));
#8316=DIRECTION('center_axis',(0.,1.,0.));
#8317=DIRECTION('ref_axis',(-1.,0.,0.));
#8318=DIRECTION('',(-1.,0.,0.));
#8319=DIRECTION('',(0.,0.,1.));
#8320=DIRECTION('center_axis',(0.866025403784439,0.5,0.));
#8321=DIRECTION('ref_axis',(-0.5,0.866025403784439,0.));
#8322=DIRECTION('',(-0.5,0.866025403784439,0.));
#8323=DIRECTION('',(0.,0.,1.));
#8324=DIRECTION('center_axis',(0.866025403784439,-0.5,0.));
#8325=DIRECTION('ref_axis',(0.5,0.866025403784439,0.));
#8326=DIRECTION('',(0.5,0.866025403784439,0.));
#8327=DIRECTION('center_axis',(0.,0.,1.));
#8328=DIRECTION('ref_axis',(1.,0.,0.));
#17029=CARTESIAN_POINT('',(0.,0.,0.));
#17030=CARTESIAN_POINT('Origin',(0.,0.,0.12));
#17031=CARTESIAN_POINT('',(-0.12639138516214,8.91322620741042E-5,0.00934196736194174));
#17032=CARTESIAN_POINT('',(-0.12645,1.54856587752183E-17,-5.55111512312578E-17));
#17033=CARTESIAN_POINT('',(-0.12645,1.54856587752183E-17,0.12));
#17034=CARTESIAN_POINT('',(-0.0488748409397564,0.116622692573588,0.));
#17035=CARTESIAN_POINT('Origin',(0.,0.,0.));
#17036=CARTESIAN_POINT('Ctrl Pts',(-0.0489111879062984,0.116810626195002,
1.20007714660797E-17));
#17037=CARTESIAN_POINT('Ctrl Pts',(-0.0838963038512042,0.101957324585112,
0.00240024091002088));
#17038=CARTESIAN_POINT('Ctrl Pts',(-0.11198221847721,0.0702793053867637,
0.00480048182004174));
#17039=CARTESIAN_POINT('Ctrl Pts',(-0.122072221370749,0.0336561163696377,
0.00720072273006261));
#17040=CARTESIAN_POINT('Ctrl Pts',(-0.125072637487486,0.022765653033531,
0.00791447094068899));
#17041=CARTESIAN_POINT('Ctrl Pts',(-0.126481745582665,0.0114379076904012,
0.00862821915131536));
#17042=CARTESIAN_POINT('Ctrl Pts',(-0.12639138516214,8.91322620741042E-5,
0.00934196736194174));
#17043=CARTESIAN_POINT('Origin',(0.,0.,0.12));
#17044=CARTESIAN_POINT('',(-0.126396145829628,-9.95859796292312E-5,0.0593419673619417));
#17045=CARTESIAN_POINT('',(-0.126575671592806,-7.20628672610732E-5,0.0456580326380584));
#17046=CARTESIAN_POINT('',(-0.12645,1.54856587752183E-17,0.12));
#17047=CARTESIAN_POINT('',(-0.10808967569503,-0.0656218295092665,0.));
#17048=CARTESIAN_POINT('Ctrl Pts',(-0.126575671592806,-7.20628672610732E-5,
0.0456580326380584));
#17049=CARTESIAN_POINT('Ctrl Pts',(-0.126327459688109,0.0361497101693465,
0.0433719816070355));
#17050=CARTESIAN_POINT('Ctrl Pts',(-0.109912066394173,0.0725710138228805,
0.0410859305760125));
#17051=CARTESIAN_POINT('Ctrl Pts',(-0.0824515099939393,0.0961223418729112,
0.0387998795449896));
#17052=CARTESIAN_POINT('Ctrl Pts',(-0.05137998778939,0.122770586059505,
0.036213220908657));
#17053=CARTESIAN_POINT('Ctrl Pts',(-0.00616751748104999,0.132941603485868,
0.0336265622723243));
#17054=CARTESIAN_POINT('Ctrl Pts',(0.0333172074018229,0.122176268745047,
0.0310399036359917));
#17055=CARTESIAN_POINT('Ctrl Pts',(0.0728019322846963,0.111410934004226,
0.028453244999659));
#17056=CARTESIAN_POINT('Ctrl Pts',(0.106558911742102,0.0797092470962188,
0.0258665863633264));
#17057=CARTESIAN_POINT('Ctrl Pts',(0.11981357554495,0.0409763259700822,
0.0232799277269937));
#17058=CARTESIAN_POINT('Ctrl Pts',(0.133068239347797,0.00224340484394604,
0.0206932690906611));
#17059=CARTESIAN_POINT('Ctrl Pts',(0.125820587496086,-0.0435207505003201,
0.0181066104543285));
#17060=CARTESIAN_POINT('Ctrl Pts',(0.101166903546451,-0.0762076816581678,
0.0155199518179958));
#17061=CARTESIAN_POINT('Ctrl Pts',(0.0765132195968157,-0.108894612816016,
0.0129332931816632));
#17062=CARTESIAN_POINT('Ctrl Pts',(0.0344535035492562,-0.128504319787445,
0.0103466345453306));
#17063=CARTESIAN_POINT('Ctrl Pts',(-0.00636464094143544,-0.126469737202777,
0.00775997590899791));
#17064=CARTESIAN_POINT('Ctrl Pts',(-0.0471827854321269,-0.124435154618108,
0.00517331727266527));
#17065=CARTESIAN_POINT('Ctrl Pts',(-0.0867593583659505,-0.100756282477341,
0.00258665863633259));
#17066=CARTESIAN_POINT('Ctrl Pts',(-0.108089675695031,-0.0656218295092657,
-5.55111512312578E-17));
#17067=CARTESIAN_POINT('Origin',(0.,0.,0.));
#17068=CARTESIAN_POINT('Ctrl Pts',(-0.12639138516214,8.91322620741042E-5,
0.00934196736194174));
#17069=CARTESIAN_POINT('Ctrl Pts',(-0.126154274972366,-0.0296906128949183,
0.011214877787648));
#17070=CARTESIAN_POINT('Ctrl Pts',(-0.115592373032178,-0.0596151635265703,
0.0130877882133543));
#17071=CARTESIAN_POINT('Ctrl Pts',(-0.0963650578556872,-0.0821635787359664,
0.0149606986390606));
#17072=CARTESIAN_POINT('Ctrl Pts',(-0.0698103971670931,-0.113304978845907,
0.0175473572753932));
#17073=CARTESIAN_POINT('Ctrl Pts',(-0.0267272342632827,-0.130377059081323,
0.0201340159117258));
#17074=CARTESIAN_POINT('Ctrl Pts',(0.0139574509341311,-0.125868770046104,
0.0227206745480584));
#17075=CARTESIAN_POINT('Ctrl Pts',(0.0546421361315456,-0.121360481010885,
0.0253073331843911));
#17076=CARTESIAN_POINT('Ctrl Pts',(0.0929283436225635,-0.0952718227050311,
0.0278939918207237));
#17077=CARTESIAN_POINT('Ctrl Pts',(0.112018291148455,-0.0590635258734944,
0.0304806504570564));
#17078=CARTESIAN_POINT('Ctrl Pts',(0.131108238674346,-0.0228552290419586,
0.033067309093389));
#17079=CARTESIAN_POINT('Ctrl Pts',(0.131001926235112,0.0234727063152593,
0.0356539677297216));
#17080=CARTESIAN_POINT('Ctrl Pts',(0.111741771403992,0.0595891814911641,
0.0382406263660542));
#17081=CARTESIAN_POINT('Ctrl Pts',(0.0924816165728724,0.0957056566670696,
0.0408272850023869));
#17082=CARTESIAN_POINT('Ctrl Pts',(0.0540676193498672,0.121610671661662,
0.0434139436387195));
#17083=CARTESIAN_POINT('Ctrl Pts',(0.0133639835211523,0.125930636937597,
0.0460006022750522));
#17084=CARTESIAN_POINT('Ctrl Pts',(-0.0273396523075625,0.130250602213533,
0.0485872609113848));
#17085=CARTESIAN_POINT('Ctrl Pts',(-0.0703329267419868,0.112985517770812,
0.0511739195477175));
#17086=CARTESIAN_POINT('Ctrl Pts',(-0.0967449447385466,0.0817152626609385,
0.0537605781840501));
#17087=CARTESIAN_POINT('Ctrl Pts',(-0.115741878896724,0.0592240248649833,
0.0556210412433473));
#17088=CARTESIAN_POINT('Ctrl Pts',(-0.126160906676814,0.0294875554882879,
0.0574815043026445));
#17089=CARTESIAN_POINT('Ctrl Pts',(-0.126396145829628,-9.95859796292312E-5,
0.0593419673619417));
#17090=CARTESIAN_POINT('Origin',(0.,0.,0.12));
#17091=CARTESIAN_POINT('',(-0.126529791093031,9.025049583615E-5,0.109341967361942));
#17092=CARTESIAN_POINT('',(-0.126349242904067,8.85860673823967E-5,0.0956580326380584));
#17093=CARTESIAN_POINT('',(-0.12645,1.54856587752183E-17,0.12));
#17094=CARTESIAN_POINT('Ctrl Pts',(-0.126349242904067,8.85860673823967E-5,
0.0956580326380584));
#17095=CARTESIAN_POINT('Ctrl Pts',(-0.126441591528965,0.0135570965972842,
0.0948119253946973));
#17096=CARTESIAN_POINT('Ctrl Pts',(-0.124448136217638,0.0269990101701626,
0.0939658181513361));
#17097=CARTESIAN_POINT('Ctrl Pts',(-0.120249444863787,0.0397126388809939,
0.093119710907975));
#17098=CARTESIAN_POINT('Ctrl Pts',(-0.107413505522824,0.0785798365820317,
0.0905330522716423));
#17099=CARTESIAN_POINT('Ctrl Pts',(-0.0739673525896496,0.110640458354997,
0.0879463936353097));
#17100=CARTESIAN_POINT('Ctrl Pts',(-0.0345920580258737,0.121821308595361,
0.085359734998977));
#17101=CARTESIAN_POINT('Ctrl Pts',(0.00478323653790218,0.133002158835724,
0.0827730763626444));
#17102=CARTESIAN_POINT('Ctrl Pts',(0.0500876727322792,0.123303237543486,
0.0801864177263117));
#17103=CARTESIAN_POINT('Ctrl Pts',(0.0814342209129887,0.0969820390626645,
0.077599759089979));
#17104=CARTESIAN_POINT('Ctrl Pts',(0.112780769093698,0.0706608405818426,
0.0750131004536464));
#17105=CARTESIAN_POINT('Ctrl Pts',(0.13016942926074,0.0277173649124373,
0.0724264418173139));
#17106=CARTESIAN_POINT('Ctrl Pts',(0.12596827751407,-0.0129984006283456,
0.0698397831809812));
#17107=CARTESIAN_POINT('Ctrl Pts',(0.121767125767399,-0.0537141661691284,
0.0672531245446486));
#17108=CARTESIAN_POINT('Ctrl Pts',(0.0959761621070158,-0.0922022215812886,
0.0646664659083159));
#17109=CARTESIAN_POINT('Ctrl Pts',(0.059914723710966,-0.111567668284471,
0.0620798072719833));
#17110=CARTESIAN_POINT('Ctrl Pts',(0.0238532853149157,-0.130933114987654,
0.0594931486356506));
#17111=CARTESIAN_POINT('Ctrl Pts',(-0.0224786278168013,-0.131175952981858,
0.056906489999318));
#17112=CARTESIAN_POINT('Ctrl Pts',(-0.0587401909579078,-0.112190380850839,
0.0543198313629853));
#17113=CARTESIAN_POINT('Ctrl Pts',(-0.0950017540990138,-0.0932048087198191,
0.0517331727266527));
#17114=CARTESIAN_POINT('Ctrl Pts',(-0.12119296724951,-0.0549908264635757,
0.0491465140903201));
#17115=CARTESIAN_POINT('Ctrl Pts',(-0.125823286774378,-0.0143210998620416,
0.0465598554539874));
#17116=CARTESIAN_POINT('Ctrl Pts',(-0.126361397696569,-0.0095946821776348,
0.0462592478486778));
#17117=CARTESIAN_POINT('Ctrl Pts',(-0.12660831057823,-0.00483509759607578,
0.0459586402433681));
#17118=CARTESIAN_POINT('Ctrl Pts',(-0.126575671592806,-7.20628672610732E-5,
0.0456580326380584));
#17119=CARTESIAN_POINT('Ctrl Pts',(-0.126396145829628,-9.95859796292312E-5,
0.0593419673619417));
#17120=CARTESIAN_POINT('Ctrl Pts',(-0.12648796685852,-0.0116483513064931,
0.0600681629389771));
#17121=CARTESIAN_POINT('Ctrl Pts',(-0.125028206814926,-0.0231743653405588,
0.0607943585160125));
#17122=CARTESIAN_POINT('Ctrl Pts',(-0.121921363946098,-0.034237873926493,
0.0615205540930479));
#17123=CARTESIAN_POINT('Ctrl Pts',(-0.110855003598394,-0.0736453296270277,
0.0641072127293806));
#17124=CARTESIAN_POINT('Ctrl Pts',(-0.0788915213442898,-0.107184815251071,
0.0666938713657133));
#17125=CARTESIAN_POINT('Ctrl Pts',(-0.0400617348236378,-0.120133683626334,
0.069280530002046));
#17126=CARTESIAN_POINT('Ctrl Pts',(-0.00123194830298627,-0.133082552001597,
0.0718671886383786));
#17127=CARTESIAN_POINT('Ctrl Pts',(0.0444641424842127,-0.125440803128081,
0.0744538472747112));
#17128=CARTESIAN_POINT('Ctrl Pts',(0.0769682295152699,-0.100563001286921,
0.0770405059110438));
#17129=CARTESIAN_POINT('Ctrl Pts',(0.109472316546327,-0.0756851994457607,
0.0796271645473764));
#17130=CARTESIAN_POINT('Ctrl Pts',(0.128784399821243,-0.0335713446369571,
0.0822138231837091));
#17131=CARTESIAN_POINT('Ctrl Pts',(0.126427276285523,0.00729262199647547,
0.0848004818200417));
#17132=CARTESIAN_POINT('Ctrl Pts',(0.124070152749803,0.0481565886299079,
0.0873871404563744));
#17133=CARTESIAN_POINT('Ctrl Pts',(0.100043822403448,0.0877706670879697,
0.0899737990927071));
#17134=CARTESIAN_POINT('Ctrl Pts',(0.0648947831756147,0.108746049780439,
0.0925604577290397));
#17135=CARTESIAN_POINT('Ctrl Pts',(0.0297457439477817,0.129721432472907,
0.0951471163653723));
#17136=CARTESIAN_POINT('Ctrl Pts',(-0.0165260041615291,0.132058119399784,
0.0977337750017049));
#17137=CARTESIAN_POINT('Ctrl Pts',(-0.0536093211433369,0.114730442741844,
0.100320433638038));
#17138=CARTESIAN_POINT('Ctrl Pts',(-0.0906926381251451,0.0974027660839045,
0.10290709227437));
#17139=CARTESIAN_POINT('Ctrl Pts',(-0.11858752397945,0.0604107258411485,
0.105493750910703));
#17140=CARTESIAN_POINT('Ctrl Pts',(-0.12504939731921,0.0199921027543164,
0.108080409547035));
#17141=CARTESIAN_POINT('Ctrl Pts',(-0.126099919499473,0.0134211506765118,
0.108500928818671));
#17142=CARTESIAN_POINT('Ctrl Pts',(-0.126583971845017,0.00675963476331471,
0.108921448090306));
#17143=CARTESIAN_POINT('Ctrl Pts',(-0.126529791093031,9.025049583615E-5,
0.109341967361942));
#17144=CARTESIAN_POINT('Origin',(0.,0.,0.12));
#17145=CARTESIAN_POINT('',(-0.126296536029262,-6.10717992316628E-5,0.159341967361942));
#17146=CARTESIAN_POINT('',(-0.126453631260982,-0.000102348163238207,0.145658032638058));
#17147=CARTESIAN_POINT('',(-0.12645,1.54856587752183E-17,0.12));
#17148=CARTESIAN_POINT('Ctrl Pts',(-0.126453631260982,-0.000102348163238207,
0.145658032638058));
#17149=CARTESIAN_POINT('Ctrl Pts',(-0.126183364177612,0.031552920325249,
0.143665210546026));
#17150=CARTESIAN_POINT('Ctrl Pts',(-0.114073771100105,0.0633928690595716,
0.141672388453994));
#17151=CARTESIAN_POINT('Ctrl Pts',(-0.0925489356314354,0.0864391430514358,
0.139679566361962));
#17152=CARTESIAN_POINT('Ctrl Pts',(-0.0646099631645552,0.116352924063146,
0.13709290772563));
#17153=CARTESIAN_POINT('Ctrl Pts',(-0.0208084524006029,0.131451366650306,
0.134506249089297));
#17154=CARTESIAN_POINT('Ctrl Pts',(0.0196287675426836,0.125106932552633,
0.131919590452964));
#17155=CARTESIAN_POINT('Ctrl Pts',(0.0600659874859703,0.11876249845496,
0.129332931816632));
#17156=CARTESIAN_POINT('Ctrl Pts',(0.097138916608591,0.0909751876724545,
0.126746273180299));
#17157=CARTESIAN_POINT('Ctrl Pts',(0.114574233156503,0.0539423598350403,
0.124159614543967));
#17158=CARTESIAN_POINT('Ctrl Pts',(0.132009549704415,0.0169095319976262,
0.121572955907634));
#17159=CARTESIAN_POINT('Ctrl Pts',(0.129807253677619,-0.0293688128946969,
0.118986297271301));
#17160=CARTESIAN_POINT('Ctrl Pts',(0.108934072954415,-0.0645786240759305,
0.116399638634969));
#17161=CARTESIAN_POINT('Ctrl Pts',(0.0880608922312115,-0.099788435257164,
0.113812979998636));
#17162=CARTESIAN_POINT('Ctrl Pts',(0.0485168268116012,-0.123929712727308,
0.111226321362303));
#17163=CARTESIAN_POINT('Ctrl Pts',(0.00765986125275547,-0.126405537442516,
0.108639662725971));
#17164=CARTESIAN_POINT('Ctrl Pts',(-0.0331971043060904,-0.128881362157723,
0.106053004089638));
#17165=CARTESIAN_POINT('Ctrl Pts',(-0.0753669700041717,-0.109691734117994,
0.103466345453305));
#17166=CARTESIAN_POINT('Ctrl Pts',(-0.100339039978837,-0.0772600332835736,
0.100879686816973));
#17167=CARTESIAN_POINT('Ctrl Pts',(-0.117142637704978,-0.0554368822612891,
0.0991391354240014));
#17168=CARTESIAN_POINT('Ctrl Pts',(-0.126159269908366,-0.0276178718881664,
0.0973985840310299));
#17169=CARTESIAN_POINT('Ctrl Pts',(-0.126349242904067,8.85860673823967E-5,
0.0956580326380584));
#17170=CARTESIAN_POINT('Ctrl Pts',(-0.126529791093031,9.025049583615E-5,
0.109341967361942));
#17171=CARTESIAN_POINT('Ctrl Pts',(-0.126250700293628,-0.0342644551610371,
0.111508106726639));
#17172=CARTESIAN_POINT('Ctrl Pts',(-0.111690189779818,-0.0688279388928191,
0.113674246091336));
#17173=CARTESIAN_POINT('Ctrl Pts',(-0.0867076257192948,-0.092297473337895,
0.115840385456033));
#17174=CARTESIAN_POINT('Ctrl Pts',(-0.0568751199544048,-0.120323220412367,
0.118427044092366));
#17175=CARTESIAN_POINT('Ctrl Pts',(-0.0121812475994092,-0.132529508630403,
0.121013702728699));
#17176=CARTESIAN_POINT('Ctrl Pts',(0.0277554439013372,-0.123558363290506,
0.123600361365031));
#17177=CARTESIAN_POINT('Ctrl Pts',(0.0676921354020838,-0.114587217950609,
0.126187020001364));
#17178=CARTESIAN_POINT('Ctrl Pts',(0.102871646048582,-0.0844386390527785,
0.128773678637697));
#17179=CARTESIAN_POINT('Ctrl Pts',(0.117851793294146,-0.0463464242807743,
0.131360337274029));
#17180=CARTESIAN_POINT('Ctrl Pts',(0.13283194053971,-0.00825420950877041,
0.133946995910362));
#17181=CARTESIAN_POINT('Ctrl Pts',(0.127612724384341,0.0377816411374068,
0.136533654546694));
#17182=CARTESIAN_POINT('Ctrl Pts',(0.104485135941302,0.0715534408109559,
0.139120313183027));
#17183=CARTESIAN_POINT('Ctrl Pts',(0.0813575474982633,0.105325240484505,
0.14170697181936));
#17184=CARTESIAN_POINT('Ctrl Pts',(0.0403215867675544,0.126832989185426,
0.144293630455692));
#17185=CARTESIAN_POINT('Ctrl Pts',(-0.000609841963000384,0.126635909896556,
0.146880289092025));
#17186=CARTESIAN_POINT('Ctrl Pts',(-0.0415412706935549,0.126438830607686,
0.149466947728358));
#17187=CARTESIAN_POINT('Ctrl Pts',(-0.0823681674239554,0.104536923329025,
0.15205360636469));
#17188=CARTESIAN_POINT('Ctrl Pts',(-0.10516942503222,0.0705438627883669,
0.154640265001023));
#17189=CARTESIAN_POINT('Ctrl Pts',(-0.118984510025511,0.0499477610899654,
0.156207499121329));
#17190=CARTESIAN_POINT('Ctrl Pts',(-0.126182304652747,0.0249129445447297,
0.157774733241635));
#17191=CARTESIAN_POINT('Ctrl Pts',(-0.126296536029262,-6.10717992316628E-5,
0.159341967361942));
#17192=CARTESIAN_POINT('Origin',(0.,0.,0.12));
#17193=CARTESIAN_POINT('',(-0.126625441102054,2.7778768752873E-5,0.209341967361942));
#17194=CARTESIAN_POINT('',(-0.126471935391749,0.000101176582396995,0.195658032638058));
#17195=CARTESIAN_POINT('',(-0.12645,1.54856587752183E-17,0.12));
#17196=CARTESIAN_POINT('',(0.0958116152722397,0.0825211298936481,0.24));
#17197=CARTESIAN_POINT('Ctrl Pts',(-0.126625441102054,2.7778768752873E-5,
0.209341967361942));
#17198=CARTESIAN_POINT('Ctrl Pts',(-0.126482885932031,-0.0388928622545336,
0.21180133566563));
#17199=CARTESIAN_POINT('Ctrl Pts',(-0.107125339127294,-0.077921419747323,
0.214260703969318));
#17200=CARTESIAN_POINT('Ctrl Pts',(-0.0759952538809665,-0.101287130411732,
0.216720072273006));
#17201=CARTESIAN_POINT('Ctrl Pts',(-0.0432539585932993,-0.12586218783339,
0.219306730909339));
#17202=CARTESIAN_POINT('Ctrl Pts',(0.0025100419330305,-0.133111106253138,
0.221893389545672));
#17203=CARTESIAN_POINT('Ctrl Pts',(0.0412155518054008,-0.119764891216682,
0.224480048182004));
#17204=CARTESIAN_POINT('Ctrl Pts',(0.0799210616777711,-0.106418676180227,
0.227066706818337));
#17205=CARTESIAN_POINT('Ctrl Pts',(0.111568080896182,-0.072477327687567,
0.229653365454669));
#17206=CARTESIAN_POINT('Ctrl Pts',(0.122246574267713,-0.0330282462555153,
0.232240024091002));
#17207=CARTESIAN_POINT('Ctrl Pts',(0.132925067639245,0.00642083517653631,
0.234826682727335));
#17208=CARTESIAN_POINT('Ctrl Pts',(0.122635035163896,0.0513776495479799,
0.237413341363667));
#17209=CARTESIAN_POINT('Ctrl Pts',(0.0958116152722397,0.0825211298936481,
0.24));
#17210=CARTESIAN_POINT('',(-0.0959791030802601,0.0826138105732953,0.24));
#17211=CARTESIAN_POINT('Origin',(0.,0.,0.24));
#17212=CARTESIAN_POINT('Ctrl Pts',(-0.0959791030802601,0.0826138105732953,
0.24));
#17213=CARTESIAN_POINT('Ctrl Pts',(-0.0710417758635208,0.111296717646776,
0.237599759089979));
#17214=CARTESIAN_POINT('Ctrl Pts',(-0.0322351762885183,0.128218895525122,
0.235199518179958));
#17215=CARTESIAN_POINT('Ctrl Pts',(0.00571352152256588,0.126497857083363,
0.232799277269937));
#17216=CARTESIAN_POINT('Ctrl Pts',(0.0466095526337785,0.124643152028446,
0.230212618633605));
#17217=CARTESIAN_POINT('Ctrl Pts',(0.0865092470399708,0.101136876245298,
0.227625959997272));
#17218=CARTESIAN_POINT('Ctrl Pts',(0.107920636628548,0.0662586835305903,
0.225039301360939));
#17219=CARTESIAN_POINT('Ctrl Pts',(0.129332026217125,0.0313804908158828,
0.222452642724607));
#17220=CARTESIAN_POINT('Ctrl Pts',(0.132255110988087,-0.014869618830384,
0.219865984088274));
#17221=CARTESIAN_POINT('Ctrl Pts',(0.115395215428634,-0.0521699181865619,
0.217279325451942));
#17222=CARTESIAN_POINT('Ctrl Pts',(0.0985353198691812,-0.0894702175427398,
0.214692666815609));
#17223=CARTESIAN_POINT('Ctrl Pts',(0.0618924439793129,-0.117820706608829,
0.212106008179276));
#17224=CARTESIAN_POINT('Ctrl Pts',(0.0215571925812854,-0.12478734248304,
0.209519349542944));
#17225=CARTESIAN_POINT('Ctrl Pts',(-0.0187780588167422,-0.13175397835725,
0.206932690906611));
#17226=CARTESIAN_POINT('Ctrl Pts',(-0.0628056857229291,-0.117336761039583,
0.204346032270278));
#17227=CARTESIAN_POINT('Ctrl Pts',(-0.0912027768750998,-0.0878586653637446,
0.201759373633946));
#17228=CARTESIAN_POINT('Ctrl Pts',(-0.113530209130371,-0.0646812849521466,
0.199725593301983));
#17229=CARTESIAN_POINT('Ctrl Pts',(-0.126194825294183,-0.0321932513395888,
0.197691812970021));
#17230=CARTESIAN_POINT('Ctrl Pts',(-0.126471935391749,0.000101176582396995,
0.195658032638058));
#17231=CARTESIAN_POINT('Origin',(0.,0.,0.350421172358873));
#17232=CARTESIAN_POINT('',(-0.154453350152392,-8.79343647196378E-5,0.0295788276411275));
#17233=CARTESIAN_POINT('',(-0.15422847552802,0.000108763211052777,0.025421172358873));
#17234=CARTESIAN_POINT('',(-0.1543,-1.01731279388251E-15,0.350421172358873));
#17235=CARTESIAN_POINT('',(0.15408394018464,-0.00816268198427004,0.));
#17236=CARTESIAN_POINT('Ctrl Pts',(-0.15422847552802,0.000108763211052763,
0.025421172358873));
#17237=CARTESIAN_POINT('Ctrl Pts',(-0.154338737393477,0.0139570514561378,
0.0247074241482466));
#17238=CARTESIAN_POINT('Ctrl Pts',(-0.146387882101843,0.0778735560251454,
0.0214070173012875));
#17239=CARTESIAN_POINT('Ctrl Pts',(-0.0581466660421577,0.171532975008042,
0.0155199518179959));
#17240=CARTESIAN_POINT('Ctrl Pts',(0.109502662757235,0.144085240745689,
0.00775997590899784));
#17241=CARTESIAN_POINT('Ctrl Pts',(0.156737212705124,0.0419221657566679,
0.00258665863633264));
#17242=CARTESIAN_POINT('Ctrl Pts',(0.15408394018464,-0.00816268198427004,
0.));
#17243=CARTESIAN_POINT('',(0.129620323775263,-0.0841289546921688,3.62607491890453E-17));
#17244=CARTESIAN_POINT('Origin',(0.,0.,0.));
#17245=CARTESIAN_POINT('Ctrl Pts',(-0.154453350152392,-8.7934364719636E-5,
0.0295788276411275));
#17246=CARTESIAN_POINT('Ctrl Pts',(-0.154150470777978,0.0441115087317509,
0.0272927766101045));
#17247=CARTESIAN_POINT('Ctrl Pts',(-0.111454882743928,0.138841433785012,
0.0224200669427489));
#17248=CARTESIAN_POINT('Ctrl Pts',(0.0476444145610997,0.174632482457551,
0.0149606986390605));
#17249=CARTESIAN_POINT('Ctrl Pts',(0.168251138196633,0.0613688951001999,
0.0073871404563744));
#17250=CARTESIAN_POINT('Ctrl Pts',(0.154676764047789,-0.0451013867871701,
0.00240024091002087));
#17251=CARTESIAN_POINT('Ctrl Pts',(0.129620323775263,-0.0841289546921688,
1.57209315010398E-17));
#17252=CARTESIAN_POINT('Origin',(0.,0.,0.350421172358873));
#17253=CARTESIAN_POINT('',(-0.154177051641736,0.000108096719625833,0.0795788276411275));
#17254=CARTESIAN_POINT('',(-0.154234284709463,-0.000121519309271207,0.075421172358873));
#17255=CARTESIAN_POINT('',(-0.1543,-1.01731279388251E-15,0.350421172358873));
#17256=CARTESIAN_POINT('Ctrl Pts',(-0.154234284709463,-0.000121519309271208,
0.0754211723588731));
#17257=CARTESIAN_POINT('Ctrl Pts',(-0.153947235272697,0.0359820467524117,
0.0735607092995758));
#17258=CARTESIAN_POINT('Ctrl Pts',(-0.123557126730793,0.122717061869437,
0.0691135876039459));
#17259=CARTESIAN_POINT('Ctrl Pts',(0.0191012565771036,0.180005302104073,
0.0620798072719832));
#17260=CARTESIAN_POINT('Ctrl Pts',(0.159724738700703,0.0851738948996701,
0.0543198313629854));
#17261=CARTESIAN_POINT('Ctrl Pts',(0.160113920417758,-0.0844204212478698,
0.0465598554539874));
#17262=CARTESIAN_POINT('Ctrl Pts',(0.0199582426985643,-0.179924098035372,
0.0387998795449896));
#17263=CARTESIAN_POINT('Ctrl Pts',(-0.123251388539896,-0.123176028715441,
0.0317536518466181));
#17264=CARTESIAN_POINT('Ctrl Pts',(-0.153939142967466,-0.0362298265692857,
0.0272940827845792));
#17265=CARTESIAN_POINT('Ctrl Pts',(-0.15422847552802,0.000108763211052763,
0.025421172358873));
#17266=CARTESIAN_POINT('Ctrl Pts',(-0.154177051641736,0.000108096719625859,
0.0795788276411275));
#17267=CARTESIAN_POINT('Ctrl Pts',(-0.154289739603949,0.0165429814548096,
0.0787327203977663));
#17268=CARTESIAN_POINT('Ctrl Pts',(-0.144420757340354,0.0830897487115299,
0.0752999545180725));
#17269=CARTESIAN_POINT('Ctrl Pts',(-0.0494457976037486,0.174130301808973,
0.0692805300020459));
#17270=CARTESIAN_POINT('Ctrl Pts',(0.11640175885633,0.13862511662766,0.061520554093048));
#17271=CARTESIAN_POINT('Ctrl Pts',(0.18005704388064,-0.0185795878987759,
0.0537605781840501));
#17272=CARTESIAN_POINT('Ctrl Pts',(0.0856431484406112,-0.159474177462153,
0.0460006022750521));
#17273=CARTESIAN_POINT('Ctrl Pts',(-0.0839657292871194,-0.160363143120653,
0.0382406263660544));
#17274=CARTESIAN_POINT('Ctrl Pts',(-0.151599316432495,-0.0616831513139142,
0.0327667014880793));
#17275=CARTESIAN_POINT('Ctrl Pts',(-0.154493177716258,-0.00590000442131094,
0.0298794352464371));
#17276=CARTESIAN_POINT('Ctrl Pts',(-0.154453350152392,-8.7934364719636E-5,
0.0295788276411275));
#17277=CARTESIAN_POINT('Origin',(0.,0.,0.350421172358873));
#17278=CARTESIAN_POINT('',(-0.154304431028624,-0.000124889850439479,0.129578827641127));
#17279=CARTESIAN_POINT('',(-0.154397364694779,0.000110127730384366,0.125421172358873));
#17280=CARTESIAN_POINT('',(-0.1543,-1.01731279388251E-15,0.350421172358873));
#17281=CARTESIAN_POINT('Ctrl Pts',(-0.154397364694779,0.000110127730384357,
0.125421172358873));
#17282=CARTESIAN_POINT('Ctrl Pts',(-0.154463478494948,0.00824841157753406,
0.125000653087238));
#17283=CARTESIAN_POINT('Ctrl Pts',(-0.150239588102603,0.0663774823757793,
0.121993475179269));
#17284=CARTESIAN_POINT('Ctrl Pts',(-0.0766286530280003,0.163994611436961,
0.116399638634969));
#17285=CARTESIAN_POINT('Ctrl Pts',(0.0927599764682439,0.155440618724813,
0.108639662725971));
#17286=CARTESIAN_POINT('Ctrl Pts',(0.180714016146597,0.0104239566588842,
0.100879686816973));
#17287=CARTESIAN_POINT('Ctrl Pts',(0.11001758793024,-0.143743725357685,
0.093119710907975));
#17288=CARTESIAN_POINT('Ctrl Pts',(-0.0572637123892103,-0.171718146500831,
0.0853597349989769));
#17289=CARTESIAN_POINT('Ctrl Pts',(-0.146220320052713,-0.0783754111826042,
0.0794602221492764));
#17290=CARTESIAN_POINT('Ctrl Pts',(-0.154346328875204,-0.0142138442593302,
0.0761473679359084));
#17291=CARTESIAN_POINT('Ctrl Pts',(-0.154234284709463,-0.000121519309271208,
0.0754211723588731));
#17292=CARTESIAN_POINT('Ctrl Pts',(-0.154304431028624,-0.000124889850439474,
0.129578827641127));
#17293=CARTESIAN_POINT('Ctrl Pts',(-0.153974638929265,0.0385022981904757,
0.127586005549095));
#17294=CARTESIAN_POINT('Ctrl Pts',(-0.120018027207353,0.127784966030512,
0.123006524820731));
#17295=CARTESIAN_POINT('Ctrl Pts',(0.0280571680938306,0.178826694862324,
0.115840385456033));
#17296=CARTESIAN_POINT('Ctrl Pts',(0.163771354656592,0.0771047007047774,
0.108080409547035));
#17297=CARTESIAN_POINT('Ctrl Pts',(0.155709331479018,-0.0923080778690166,
0.100320433638038));
#17298=CARTESIAN_POINT('Ctrl Pts',(0.0109489686262093,-0.180682908560435,
0.0925604577290397));
#17299=CARTESIAN_POINT('Ctrl Pts',(-0.126591758993125,-0.118094248159534,
0.0856465890634029));
#17300=CARTESIAN_POINT('Ctrl Pts',(-0.153945238013925,-0.0337005743957639,
0.0813193790340989));
#17301=CARTESIAN_POINT('Ctrl Pts',(-0.154177051641736,0.000108096719625859,
0.0795788276411275));
#17302=CARTESIAN_POINT('Origin',(0.,0.,0.350421172358873));
#17303=CARTESIAN_POINT('',(-0.154326766555531,0.000123460234585843,0.179578827641127));
#17304=CARTESIAN_POINT('',(-0.154112736333057,-7.45225671948511E-5,0.175421172358873));
#17305=CARTESIAN_POINT('',(-0.1543,-1.01731279388251E-15,0.350421172358873));
#17306=CARTESIAN_POINT('Ctrl Pts',(-0.154112736333057,-7.45225671948471E-5,
0.175421172358873));
#17307=CARTESIAN_POINT('Ctrl Pts',(-0.153973346049181,0.0303998999070902,
0.173853938238567));
#17308=CARTESIAN_POINT('Ctrl Pts',(-0.130694151755309,0.111367805862998,
0.169700045481928));
#17309=CARTESIAN_POINT('Ctrl Pts',(-0.000871711368246156,0.181012066871201,
0.162959494088956));
#17310=CARTESIAN_POINT('Ctrl Pts',(0.149350085565286,0.102277888352765,
0.155199518179958));
#17311=CARTESIAN_POINT('Ctrl Pts',(0.168456255263351,-0.0662471829332422,
0.14743954227096));
#17312=CARTESIAN_POINT('Ctrl Pts',(0.0396733728729688,-0.17661315503135,
0.139679566361963));
#17313=CARTESIAN_POINT('Ctrl Pts',(-0.115072782317819,-0.134350623919955,
0.1323401097246));
#17314=CARTESIAN_POINT('Ctrl Pts',(-0.154056805498669,-0.041811035439686,
0.12758731172357));
#17315=CARTESIAN_POINT('Ctrl Pts',(-0.154397364694779,0.000110127730384357,
0.125421172358873));
#17316=CARTESIAN_POINT('Ctrl Pts',(-0.154326766555531,0.000123460234585825,
0.179578827641127));
#17317=CARTESIAN_POINT('Ctrl Pts',(-0.154418689716183,0.0108361910665024,
0.179025949336757));
#17318=CARTESIAN_POINT('Ctrl Pts',(-0.148597337680631,0.071569631208062,
0.175886412396054));
#17319=CARTESIAN_POINT('Ctrl Pts',(-0.0683530255288039,0.167611467503216,
0.170160216819019));
#17320=CARTESIAN_POINT('Ctrl Pts',(0.100397202365132,0.150621028353064,
0.162400240910021));
#17321=CARTESIAN_POINT('Ctrl Pts',(0.18100910679194,0.00139719974911195,
0.154640265001023));
#17322=CARTESIAN_POINT('Ctrl Pts',(0.102711092909207,-0.149052183789333,
0.146880289092025));
#17323=CARTESIAN_POINT('Ctrl Pts',(-0.0657574679958034,-0.168648048308422,
0.139120313183027));
#17324=CARTESIAN_POINT('Ctrl Pts',(-0.148058381688037,-0.0731761882111772,
0.133353159366061));
#17325=CARTESIAN_POINT('Ctrl Pts',(-0.154402705029802,-0.0116353181791797,
0.130172664185428));
#17326=CARTESIAN_POINT('Ctrl Pts',(-0.154304431028624,-0.000124889850439474,
0.129578827641127));
#17327=CARTESIAN_POINT('Origin',(0.,0.,0.350421172358873));
#17328=CARTESIAN_POINT('',(-0.154128406284035,-0.000157308197905263,0.229578827641128));
#17329=CARTESIAN_POINT('',(-0.154514081154978,3.38969080117728E-5,0.225421172358873));
#17330=CARTESIAN_POINT('',(-0.1543,-1.01731279388251E-15,0.350421172358873));
#17331=CARTESIAN_POINT('',(-0.0398513841857245,-0.149064942821851,0.24));
#17332=CARTESIAN_POINT('Ctrl Pts',(-0.0398513841857245,-0.149064942821851,
0.24));
#17333=CARTESIAN_POINT('Ctrl Pts',(-0.0883048112969314,-0.136111285829332,
0.237413341363667));
#17334=CARTESIAN_POINT('Ctrl Pts',(-0.143745772087175,-0.0847488633265083,
0.233939617244043));
#17335=CARTESIAN_POINT('Ctrl Pts',(-0.154234229255939,-0.017399338864059,
0.230465893124419));
#17336=CARTESIAN_POINT('Ctrl Pts',(-0.154128406284035,-0.00015730819790527,
0.229578827641128));
#17337=CARTESIAN_POINT('',(0.0399565498027962,-0.149273502906638,0.24));
#17338=CARTESIAN_POINT('Origin',(0.,0.,0.24));
#17339=CARTESIAN_POINT('Ctrl Pts',(0.0399565498027963,-0.149273502906638,
0.24));
#17340=CARTESIAN_POINT('Ctrl Pts',(-0.00490373130458673,-0.161043406468747,
0.237599759089979));
#17341=CARTESIAN_POINT('Ctrl Pts',(-0.107666111297752,-0.141562671532916,
0.23274014987627));
#17342=CARTESIAN_POINT('Ctrl Pts',(-0.154340128899266,-0.0474588267763927,
0.227880540662561));
#17343=CARTESIAN_POINT('Ctrl Pts',(-0.154514081154978,3.3896908011755E-5,
0.225421172358873));
#17344=CARTESIAN_POINT('Origin',(0.,0.,0.350421172358873));
#17345=CARTESIAN_POINT('Ctrl Pts',(-0.154514081154978,3.3896908011755E-5,
0.225421172358873));
#17346=CARTESIAN_POINT('Ctrl Pts',(-0.154523084458981,0.00249199339844659,
0.225293882026228));
#17347=CARTESIAN_POINT('Ctrl Pts',(-0.153375868586475,0.0548933889046004,
0.222579933057251));
#17348=CARTESIAN_POINT('Ctrl Pts',(-0.0942515706791253,0.154556313135293,
0.217279325451942));
#17349=CARTESIAN_POINT('Ctrl Pts',(0.0750450248431312,0.164716481511431,
0.209519349542944));
#17350=CARTESIAN_POINT('Ctrl Pts',(0.178461260043253,0.0303012077178856,
0.201759373633945));
#17351=CARTESIAN_POINT('Ctrl Pts',(0.125203781387627,-0.130731709675357,
0.193999397724948));
#17352=CARTESIAN_POINT('Ctrl Pts',(-0.0379704533096903,-0.17698585337688,
0.18623942181595));
#17353=CARTESIAN_POINT('Ctrl Pts',(-0.141587477595567,-0.0899051669249145,
0.180046680027258));
#17354=CARTESIAN_POINT('Ctrl Pts',(-0.154203404262525,-0.019896942829432,
0.176440596874899));
#17355=CARTESIAN_POINT('Ctrl Pts',(-0.154112736333057,-7.45225671948471E-5,
0.175421172358873));
#17356=CARTESIAN_POINT('Ctrl Pts',(-0.154128406284035,-0.00015730819790527,
0.229578827641128));
#17357=CARTESIAN_POINT('Ctrl Pts',(-0.153925652370292,0.0328779499839183,
0.227879234488086));
#17358=CARTESIAN_POINT('Ctrl Pts',(-0.127638532780061,0.116591914860373,
0.223592982698713));
#17359=CARTESIAN_POINT('Ctrl Pts',(0.00818767200092134,0.180778621679153,
0.216720072273006));
#17360=CARTESIAN_POINT('Ctrl Pts',(0.154249898498561,0.0947283641859207,
0.208960096364008));
#17361=CARTESIAN_POINT('Ctrl Pts',(0.164950538597243,-0.0745810526211722,
0.201200120455011));
#17362=CARTESIAN_POINT('Ctrl Pts',(0.0308106631569891,-0.178364693496558,
0.193440144546012));
#17363=CARTESIAN_POINT('Ctrl Pts',(-0.118879635670858,-0.129347344159377,
0.186233046941385));
#17364=CARTESIAN_POINT('Ctrl Pts',(-0.153988624301243,-0.0392836590090855,
0.18161260797309));
#17365=CARTESIAN_POINT('Ctrl Pts',(-0.154326766555531,0.000123460234585825,
0.179578827641127));
#17366=CARTESIAN_POINT('Ctrl Pts',(0.0958116152722397,0.0825211298936481,
0.24));
#17367=CARTESIAN_POINT('Ctrl Pts',(0.122635035163896,0.0513776495479799,
0.237413341363667));
#17368=CARTESIAN_POINT('Ctrl Pts',(0.143215100114593,-0.0385359791949074,
0.232240024091002));
#17369=CARTESIAN_POINT('Ctrl Pts',(0.0482740424593604,-0.140360024672886,
0.224480048182004));
#17370=CARTESIAN_POINT('Ctrl Pts',(-0.0890179591196291,-0.118613269413641,
0.216720072273006));
#17371=CARTESIAN_POINT('Ctrl Pts',(-0.148173729266643,0.00709031985706173,
0.208960096364008));
#17372=CARTESIAN_POINT('Ctrl Pts',(-0.0772398646297824,0.126660050524678,
0.20120012045501));
#17373=CARTESIAN_POINT('Ctrl Pts',(0.0614999571705377,0.134986384232796,
0.193440144546013));
#17374=CARTESIAN_POINT('Ctrl Pts',(0.146250332679645,0.0248320655601208,
0.185680168637014));
#17375=CARTESIAN_POINT('Ctrl Pts',(0.102605431992647,-0.107135610424167,
0.177920192728017));
#17376=CARTESIAN_POINT('Ctrl Pts',(-0.0311170694815965,-0.145041225920327,
0.170160216819019));
#17377=CARTESIAN_POINT('Ctrl Pts',(-0.137521919612742,-0.0556176253575994,
0.162400240910021));
#17378=CARTESIAN_POINT('Ctrl Pts',(-0.123195064154356,0.0826350160503635,
0.154640265001023));
#17379=CARTESIAN_POINT('Ctrl Pts',(-0.000714373963154436,0.148340737886347,
0.146880289092025));
#17380=CARTESIAN_POINT('Ctrl Pts',(0.122393508228972,0.0838174917835845,
0.139120313183027));
#17381=CARTESIAN_POINT('Ctrl Pts',(0.138051156695079,-0.0542900601549481,
0.131360337274029));
#17382=CARTESIAN_POINT('Ctrl Pts',(0.032512624755586,-0.14473579684844,
0.123600361365031));
#17383=CARTESIAN_POINT('Ctrl Pts',(-0.101568992309399,-0.108116932194331,
0.115840385456033));
#17384=CARTESIAN_POINT('Ctrl Pts',(-0.146482409833755,0.0234186855983926,
0.108080409547036));
#17385=CARTESIAN_POINT('Ctrl Pts',(-0.0627977522708403,0.13439480632666,
0.100320433638038));
#17386=CARTESIAN_POINT('Ctrl Pts',(0.076017492057093,0.127384745546031,
0.0925604577290397));
#17387=CARTESIAN_POINT('Ctrl Pts',(0.148096483096158,0.00854251017184644,
0.0848004818200417));
#17388=CARTESIAN_POINT('Ctrl Pts',(0.0901602332714121,-0.117799054254564,
0.0770405059110438));
#17389=CARTESIAN_POINT('Ctrl Pts',(-0.0469280390901857,-0.140724300875114,
0.069280530002046));
#17390=CARTESIAN_POINT('Ctrl Pts',(-0.142818485852497,-0.0401058440029853,
0.0615205540930479));
#17391=CARTESIAN_POINT('Ctrl Pts',(-0.113326201176411,0.0957204333280909,
0.0537605781840501));
#17392=CARTESIAN_POINT('Ctrl Pts',(0.0156536221268617,0.147515686656254,
0.0460006022750521));
#17393=CARTESIAN_POINT('Ctrl Pts',(0.130895613795878,0.0698006416724775,
0.0382406263660543));
#17394=CARTESIAN_POINT('Ctrl Pts',(0.13121455111358,-0.0691831643991777,
0.0304806504570563));
#17395=CARTESIAN_POINT('Ctrl Pts',(0.0163559286405278,-0.147449139316739,
0.0227206745480584));
#17396=CARTESIAN_POINT('Ctrl Pts',(-0.112893560070904,-0.0962328986104914,
0.0149606986390606));
#17397=CARTESIAN_POINT('Ctrl Pts',(-0.142972035491037,0.0393992613429074,
0.00720072273006258));
#17398=CARTESIAN_POINT('Ctrl Pts',(-0.0476516261894416,0.140572551456688,
-0.000559253178935252));
#17399=CARTESIAN_POINT('Ctrl Pts',(0.0897382482543901,0.118078928660352,
-0.00831922908793326));
#17400=CARTESIAN_POINT('Ctrl Pts',(0.128447313976429,0.0343555272840613,
-0.0134925463605985));
#17401=CARTESIAN_POINT('Ctrl Pts',(0.126272937371016,-0.00668937872268922,
-0.0160792049969311));
#17402=CARTESIAN_POINT('Ctrl Pts',(0.102845629995666,0.0885794229410663,
0.245359734998977));
#17403=CARTESIAN_POINT('Ctrl Pts',(0.13163829265517,0.0551495423644061,
0.242773076362644));
#17404=CARTESIAN_POINT('Ctrl Pts',(0.153729244145676,-0.0413651001137901,
0.237599759089979));
#17405=CARTESIAN_POINT('Ctrl Pts',(0.0518180837997932,-0.150664563191773,
0.229839783180981));
#17406=CARTESIAN_POINT('Ctrl Pts',(-0.0955532172229155,-0.127321268762976,
0.222079807271983));
#17407=CARTESIAN_POINT('Ctrl Pts',(-0.159051911315084,0.00761085605850937,
0.214319831362985));
#17408=CARTESIAN_POINT('Ctrl Pts',(-0.0829104333128967,0.135958804728216,
0.206559855453988));
#17409=CARTESIAN_POINT('Ctrl Pts',(0.0660149797280689,0.144896416659008,
0.19879987954499));
#17410=CARTESIAN_POINT('Ctrl Pts',(0.156987308467515,0.0266551129460425,
0.191039903635992));
#17411=CARTESIAN_POINT('Ctrl Pts',(0.110138215124307,-0.11500097684123,
0.183279927726994));
#17412=CARTESIAN_POINT('Ctrl Pts',(-0.0334015307576278,-0.155689435072511,
0.175519951817996));
#17413=CARTESIAN_POINT('Ctrl Pts',(-0.147618098500879,-0.0597007962188336,
0.167759975908998));
#17414=CARTESIAN_POINT('Ctrl Pts',(-0.13223943620312,0.0887016700559064,
0.16));
#17415=CARTESIAN_POINT('Ctrl Pts',(-0.000766819764851659,0.159231180881298,
0.152240024091002));
#17416=CARTESIAN_POINT('Ctrl Pts',(0.131379034007743,0.0899709573066447,
0.144480048182004));
#17417=CARTESIAN_POINT('Ctrl Pts',(0.14818618955117,-0.0582757677477129,
0.136720072273006));
#17418=CARTESIAN_POINT('Ctrl Pts',(0.0348995407947136,-0.15536158290941,
0.128960096364009));
#17419=CARTESIAN_POINT('Ctrl Pts',(-0.109025685167754,-0.116054342400242,
0.12120012045501));
#17420=CARTESIAN_POINT('Ctrl Pts',(-0.157236423577976,0.0251379696208395,
0.113440144546013));
#17421=CARTESIAN_POINT('Ctrl Pts',(-0.0674080525232269,0.144261408030094,
0.105680168637014));
#17422=CARTESIAN_POINT('Ctrl Pts',(0.0815983201941432,0.136736703272292,
0.0979201927280168));
#17423=CARTESIAN_POINT('Ctrl Pts',(0.158968994112971,0.00916965900085902,
0.0901602168190187));
#17424=CARTESIAN_POINT('Ctrl Pts',(0.0967793514910216,-0.126447277955604,
0.0824002409100209));
#17425=CARTESIAN_POINT('Ctrl Pts',(-0.0503732635231939,-0.151055582750353,
0.0746402650010229));
#17426=CARTESIAN_POINT('Ctrl Pts',(-0.15330351242688,-0.0430502166284845,
0.066880289092025));
#17427=CARTESIAN_POINT('Ctrl Pts',(-0.121646050135849,0.102747753924341,
0.0591203131830272));
#17428=CARTESIAN_POINT('Ctrl Pts',(0.0168028336102756,0.158345558472194,
0.0513603372740292));
#17429=CARTESIAN_POINT('Ctrl Pts',(0.140505322097486,0.074925059414875,
0.0436003613650313));
#17430=CARTESIAN_POINT('Ctrl Pts',(0.140847674214973,-0.0742622500154084,
0.0358403854560334));
#17431=CARTESIAN_POINT('Ctrl Pts',(0.0175566999932067,-0.158274125556283,
0.0280804095470355));
#17432=CARTESIAN_POINT('Ctrl Pts',(-0.121181646661057,-0.103297841872129,
0.0203204336380376));
#17433=CARTESIAN_POINT('Ctrl Pts',(-0.153468334920127,0.0422917601656304,
0.0125604577290396));
#17434=CARTESIAN_POINT('Ctrl Pts',(-0.0511499728070136,0.150892692640473,
0.00480048182004178));
#17435=CARTESIAN_POINT('Ctrl Pts',(0.0963263864220051,0.126747699355464,
-0.00295949408895622));
#17436=CARTESIAN_POINT('Ctrl Pts',(0.137877280219327,0.0368777401082635,
-0.00813281136162143));
#17437=CARTESIAN_POINT('Ctrl Pts',(0.135543271642224,-0.00718047980988283,
-0.0107194699979541));
#17438=CARTESIAN_POINT('Ctrl Pts',(0.109879644719093,0.0946377159884845,
0.250719469997954));
#17439=CARTESIAN_POINT('Ctrl Pts',(0.140641550146443,0.0589214351808321,
0.248132811361621));
#17440=CARTESIAN_POINT('Ctrl Pts',(0.164243388176759,-0.0441942210326729,
0.242959494088956));
#17441=CARTESIAN_POINT('Ctrl Pts',(0.055362125140226,-0.160969101710661,
0.235199518179958));
#17442=CARTESIAN_POINT('Ctrl Pts',(-0.102088475326202,-0.13602926811231,
0.227439542270961));
#17443=CARTESIAN_POINT('Ctrl Pts',(-0.169930093363525,0.00813139225995705,
0.219679566361962));
#17444=CARTESIAN_POINT('Ctrl Pts',(-0.0885810019960112,0.145257558931755,
0.211919590452965));
#17445=CARTESIAN_POINT('Ctrl Pts',(0.0705300022856002,0.154806449085219,
0.204159614543967));
#17446=CARTESIAN_POINT('Ctrl Pts',(0.167724284255384,0.0284781603319641,
0.196399638634969));
#17447=CARTESIAN_POINT('Ctrl Pts',(0.117670998255967,-0.122866343258294,
0.188639662725971));
#17448=CARTESIAN_POINT('Ctrl Pts',(-0.0356859920336591,-0.166337644224695,
0.180879686816973));
#17449=CARTESIAN_POINT('Ctrl Pts',(-0.157714277389017,-0.0637839670800676,
0.173119710907975));
#17450=CARTESIAN_POINT('Ctrl Pts',(-0.141283808251885,0.0947683240614489,
0.165359734998977));
#17451=CARTESIAN_POINT('Ctrl Pts',(-0.000819265566548849,0.17012162387625,
0.157599759089979));
#17452=CARTESIAN_POINT('Ctrl Pts',(0.140364559786514,0.0961244228297045,
0.149839783180981));
#17453=CARTESIAN_POINT('Ctrl Pts',(0.158321222407261,-0.0622614753404775,
0.142079807271983));
#17454=CARTESIAN_POINT('Ctrl Pts',(0.0372864568338413,-0.16598736897038,
0.134319831362986));
#17455=CARTESIAN_POINT('Ctrl Pts',(-0.116482378026109,-0.123991752606152,
0.126559855453987));
#17456=CARTESIAN_POINT('Ctrl Pts',(-0.167990437322196,0.0268572536432864,
0.11879987954499));
#17457=CARTESIAN_POINT('Ctrl Pts',(-0.0720183527756138,0.154128009733527,
0.111039903635992));
#17458=CARTESIAN_POINT('Ctrl Pts',(0.0871791483311938,0.146088660998552,
0.103279927726994));
#17459=CARTESIAN_POINT('Ctrl Pts',(0.169841505129784,0.00979680782987164,
0.0955199518179957));
#17460=CARTESIAN_POINT('Ctrl Pts',(0.103398469710631,-0.135095501656644,
0.0877599759089979));
#17461=CARTESIAN_POINT('Ctrl Pts',(-0.0538184879562023,-0.161386864625592,
0.08));
#17462=CARTESIAN_POINT('Ctrl Pts',(-0.163788539001263,-0.0459945892539838,
0.0722400240910021));
#17463=CARTESIAN_POINT('Ctrl Pts',(-0.129965899095288,0.10977507452059,
0.0644800481820042));
#17464=CARTESIAN_POINT('Ctrl Pts',(0.0179520450936897,0.169175430288133,
0.0567200722730062));
#17465=CARTESIAN_POINT('Ctrl Pts',(0.150115030399095,0.0800494771572726,
0.0489600963640084));
#17466=CARTESIAN_POINT('Ctrl Pts',(0.150480797316365,-0.0793413356316391,
0.0412001204550104));
#17467=CARTESIAN_POINT('Ctrl Pts',(0.0187574713458855,-0.169099111795828,
0.0334401445460125));
#17468=CARTESIAN_POINT('Ctrl Pts',(-0.129469733251211,-0.110362785133767,
0.0256801686370146));
#17469=CARTESIAN_POINT('Ctrl Pts',(-0.163964634349217,0.0451842589883535,
0.0179201927280167));
#17470=CARTESIAN_POINT('Ctrl Pts',(-0.0546483194245858,0.161212833824257,
0.0101602168190188));
#17471=CARTESIAN_POINT('Ctrl Pts',(0.10291452458962,0.135416470050577,0.00240024091002082));
#17472=CARTESIAN_POINT('Ctrl Pts',(0.147307246462226,0.0393999529324658,
-0.00277307636264439));
#17473=CARTESIAN_POINT('Ctrl Pts',(0.144813605913432,-0.00767158089707644,
-0.00535973499897704));
#17474=CARTESIAN_POINT('Ctrl Pts',(0.116913659442519,0.100696009035903,
0.256079204996931));
#17475=CARTESIAN_POINT('Ctrl Pts',(0.149644807637716,0.0626933279972582,
0.253492546360598));
#17476=CARTESIAN_POINT('Ctrl Pts',(0.174757532207842,-0.0470233419515556,
0.248319229087933));
#17477=CARTESIAN_POINT('Ctrl Pts',(0.0589061664806588,-0.171273640229548,
0.240559253178935));
#17478=CARTESIAN_POINT('Ctrl Pts',(-0.108623733429488,-0.144737267461644,
0.232799277269938));
#17479=CARTESIAN_POINT('Ctrl Pts',(-0.180808275411966,0.00865192846140473,
0.225039301360939));
#17480=CARTESIAN_POINT('Ctrl Pts',(-0.0942515706791253,0.154556313135293,
0.217279325451942));
#17481=CARTESIAN_POINT('Ctrl Pts',(0.0750450248431312,0.164716481511431,
0.209519349542944));
#17482=CARTESIAN_POINT('Ctrl Pts',(0.178461260043253,0.0303012077178856,
0.201759373633945));
#17483=CARTESIAN_POINT('Ctrl Pts',(0.125203781387627,-0.130731709675357,
0.193999397724948));
#17484=CARTESIAN_POINT('Ctrl Pts',(-0.0379704533096903,-0.17698585337688,
0.18623942181595));
#17485=CARTESIAN_POINT('Ctrl Pts',(-0.167810456277154,-0.0678671379413016,
0.178479445906952));
#17486=CARTESIAN_POINT('Ctrl Pts',(-0.150328180300649,0.100834978066992,
0.170719469997954));
#17487=CARTESIAN_POINT('Ctrl Pts',(-0.000871711368246156,0.181012066871201,
0.162959494088956));
#17488=CARTESIAN_POINT('Ctrl Pts',(0.149350085565286,0.102277888352765,
0.155199518179958));
#17489=CARTESIAN_POINT('Ctrl Pts',(0.168456255263351,-0.0662471829332422,
0.14743954227096));
#17490=CARTESIAN_POINT('Ctrl Pts',(0.0396733728729688,-0.17661315503135,
0.139679566361963));
#17491=CARTESIAN_POINT('Ctrl Pts',(-0.123939070884463,-0.131929162812062,
0.131919590452964));
#17492=CARTESIAN_POINT('Ctrl Pts',(-0.178744451066417,0.0285765376657333,
0.124159614543967));
#17493=CARTESIAN_POINT('Ctrl Pts',(-0.0766286530280003,0.163994611436961,
0.116399638634969));
#17494=CARTESIAN_POINT('Ctrl Pts',(0.0927599764682439,0.155440618724813,
0.108639662725971));
#17495=CARTESIAN_POINT('Ctrl Pts',(0.180714016146597,0.0104239566588842,
0.100879686816973));
#17496=CARTESIAN_POINT('Ctrl Pts',(0.11001758793024,-0.143743725357685,
0.093119710907975));
#17497=CARTESIAN_POINT('Ctrl Pts',(-0.0572637123892103,-0.171718146500831,
0.0853597349989769));
#17498=CARTESIAN_POINT('Ctrl Pts',(-0.174273565575645,-0.048938961879483,
0.0775997590899791));
#17499=CARTESIAN_POINT('Ctrl Pts',(-0.138285748054726,0.11680239511684,
0.0698397831809812));
#17500=CARTESIAN_POINT('Ctrl Pts',(0.0191012565771036,0.180005302104073,
0.0620798072719832));
#17501=CARTESIAN_POINT('Ctrl Pts',(0.159724738700703,0.0851738948996701,
0.0543198313629854));
#17502=CARTESIAN_POINT('Ctrl Pts',(0.160113920417758,-0.0844204212478698,
0.0465598554539874));
#17503=CARTESIAN_POINT('Ctrl Pts',(0.0199582426985643,-0.179924098035372,
0.0387998795449896));
#17504=CARTESIAN_POINT('Ctrl Pts',(-0.137757819841364,-0.117427728395404,
0.0310399036359917));
#17505=CARTESIAN_POINT('Ctrl Pts',(-0.174460933778308,0.0480767578110765,
0.0232799277269937));
#17506=CARTESIAN_POINT('Ctrl Pts',(-0.0581466660421577,0.171532975008042,
0.0155199518179959));
#17507=CARTESIAN_POINT('Ctrl Pts',(0.109502662757235,0.144085240745689,
0.00775997590899784));
#17508=CARTESIAN_POINT('Ctrl Pts',(0.156737212705124,0.0419221657566679,
0.00258665863633264));
#17509=CARTESIAN_POINT('Ctrl Pts',(0.15408394018464,-0.00816268198427004,
0.));
#17510=CARTESIAN_POINT('Ctrl Pts',(0.15408394018464,-0.00816268198427004,
0.));
#17511=CARTESIAN_POINT('Ctrl Pts',(0.153697863146473,0.00250812953454787,
1.45220469349306E-17));
#17512=CARTESIAN_POINT('Ctrl Pts',(0.152123106309386,0.0130673133993916,
-2.32988231788825E-17));
#17513=CARTESIAN_POINT('Ctrl Pts',(0.149466152202855,0.0233620190894148,
-6.07153216591882E-17));
#17514=CARTESIAN_POINT('Ctrl Pts',(0.14793019248835,0.0293132898222067,
-8.23454409684948E-17));
#17515=CARTESIAN_POINT('Ctrl Pts',(0.146031563681721,0.0351760135160456,
3.17823908273165E-17));
#17516=CARTESIAN_POINT('Ctrl Pts',(0.143784059453749,0.0409171473780902,
6.24500451351651E-17));
#17517=CARTESIAN_POINT('Ctrl Pts',(0.142595904075608,0.0439522291322952,
7.86626679846993E-17));
#17518=CARTESIAN_POINT('Ctrl Pts',(0.141309213132582,0.0469553015723855,
1.03399090950918E-16));
#17519=CARTESIAN_POINT('Ctrl Pts',(0.13992871365498,0.0499144025840292,
1.00613961606655E-16));
#17520=CARTESIAN_POINT('Ctrl Pts',(0.135493978469587,0.0594202586791481,
9.16669744478229E-17));
#17521=CARTESIAN_POINT('Ctrl Pts',(0.130119641392827,0.0684241765595774,
5.76730757846686E-17));
#17522=CARTESIAN_POINT('Ctrl Pts',(0.123887660540245,0.0767683201192124,
1.38777878078145E-16));
#17523=CARTESIAN_POINT('Ctrl Pts',(0.120656388342022,0.0810947453345699,
1.808305895663E-16));
#17524=CARTESIAN_POINT('Ctrl Pts',(0.117193874983239,0.0852432898306738,
1.062697842984E-16));
#17525=CARTESIAN_POINT('Ctrl Pts',(0.11350808038867,0.0891875047540603,
1.14491749414469E-16));
#17526=CARTESIAN_POINT('Ctrl Pts',(0.110158526423333,0.0927719043720516,
1.21963656801269E-16));
#17527=CARTESIAN_POINT('Ctrl Pts',(0.106618991420749,0.0961915975683434,
1.17223950247179E-16));
#17528=CARTESIAN_POINT('Ctrl Pts',(0.102922970874274,0.0994011657423757,
1.02348685082632E-16));
#17529=CARTESIAN_POINT('Ctrl Pts',(0.0973787571548163,0.104215676830788,
8.00350512245867E-17));
#17530=CARTESIAN_POINT('Ctrl Pts',(0.0914754811895955,0.108568278221023,
6.56075743842472E-17));
#17531=CARTESIAN_POINT('Ctrl Pts',(0.0852365492443714,0.11239450959967,
3.29597460435593E-17));
#17532=CARTESIAN_POINT('Ctrl Pts',(0.0787787796913796,0.116354950379705,
-7.26807264206779E-19));
#17533=CARTESIAN_POINT('Ctrl Pts',(0.0719608771003193,0.11975150351845,
7.81983513604452E-17));
#17534=CARTESIAN_POINT('Ctrl Pts',(0.0648645680501024,0.122569786811788,
1.05818132034585E-16));
#17535=CARTESIAN_POINT('Ctrl Pts',(0.0619760396963809,0.123716959397427,
1.17060669392563E-16));
#17536=CARTESIAN_POINT('Ctrl Pts',(0.0590419697559043,0.124767587801255,
-1.70921410850511E-17));
#17537=CARTESIAN_POINT('Ctrl Pts',(0.0560804949635964,0.12571697313192,
-8.67361737988404E-19));
#17538=CARTESIAN_POINT('Ctrl Pts',(0.0481895916857994,0.128246627558523,
4.23638569993146E-17));
#17539=CARTESIAN_POINT('Ctrl Pts',(0.040081547172159,0.13006877931966,2.48189907303608E-17));
#17540=CARTESIAN_POINT('Ctrl Pts',(0.0318655688619291,0.131172622122806,
0.));
#17541=CARTESIAN_POINT('Ctrl Pts',(0.0267717292715239,0.131856995664207,
-1.5387571972871E-17));
#17542=CARTESIAN_POINT('Ctrl Pts',(0.0216363184326117,0.132264755542675,
5.61228976213782E-17));
#17543=CARTESIAN_POINT('Ctrl Pts',(0.0164863123329273,0.132388468809724,
3.03576608295941E-17));
#17544=CARTESIAN_POINT('Ctrl Pts',(0.0120733572364389,0.13249447666326,
8.27985532573229E-18));
#17545=CARTESIAN_POINT('Ctrl Pts',(0.00764667637530932,0.132391154756805,
7.9933444120104E-17));
#17546=CARTESIAN_POINT('Ctrl Pts',(0.00324855819595315,0.132074892239241,
9.62771529167128E-17));
#17547=CARTESIAN_POINT('Ctrl Pts',(-0.00215998367955725,0.131685971569047,
1.16375665467493E-16));
#17548=CARTESIAN_POINT('Ctrl Pts',(-0.00753310453775717,0.130975837616781,
1.12286849362194E-16));
#17549=CARTESIAN_POINT('Ctrl Pts',(-0.0128378223015392,0.129936202211006,
1.27068494615301E-16));
#17550=CARTESIAN_POINT('Ctrl Pts',(-0.0180922709275414,0.128906418710228,
1.41710064449709E-16));
#17551=CARTESIAN_POINT('Ctrl Pts',(-0.023283936630727,0.12755123862641,
1.19281234835921E-16));
#17552=CARTESIAN_POINT('Ctrl Pts',(-0.028350637156304,0.125868914531291,
9.19403442267708E-17));
#17553=CARTESIAN_POINT('Ctrl Pts',(-0.0326437071621008,0.124443463179602,
6.87741127091605E-17));
#17554=CARTESIAN_POINT('Ctrl Pts',(-0.0368509055758185,0.122782751372096,
3.08039683582783E-17));
#17555=CARTESIAN_POINT('Ctrl Pts',(-0.0409513668396969,0.120880349084932,
-1.95156391047391E-18));
#17556=CARTESIAN_POINT('Ctrl Pts',(-0.0436523616789034,0.119627226953286,
-2.45035827619675E-17));
#17557=CARTESIAN_POINT('Ctrl Pts',(-0.0463070048384274,0.118269169850402,
-4.56986185075063E-18));
#17558=CARTESIAN_POINT('Ctrl Pts',(-0.0489111879062984,0.116810626195002,
-1.73472347597681E-18));
#17559=CARTESIAN_POINT('Ctrl Pts',(0.0958116152722397,0.0825211298936481,
0.24));
#17560=CARTESIAN_POINT('Ctrl Pts',(0.102494250906434,0.0762804363331629,
0.24));
#17561=CARTESIAN_POINT('Ctrl Pts',(0.108399952301676,0.0693089192431419,
0.24));
#17562=CARTESIAN_POINT('Ctrl Pts',(0.113520383394708,0.0617855200816623,
0.24));
#17563=CARTESIAN_POINT('Ctrl Pts',(0.11760088593285,0.0557900777417299,
0.24));
#17564=CARTESIAN_POINT('Ctrl Pts',(0.1211824537664,0.0494427873910869,0.24));
#17565=CARTESIAN_POINT('Ctrl Pts',(0.124247292533427,0.0428169095598754,
0.24));
#17566=CARTESIAN_POINT('Ctrl Pts',(0.125635784531567,0.0398151273949318,
0.24));
#17567=CARTESIAN_POINT('Ctrl Pts',(0.126914357096627,0.0367636074968772,
0.24));
#17568=CARTESIAN_POINT('Ctrl Pts',(0.128080244072735,0.0336751552254939,
0.24));
#17569=CARTESIAN_POINT('Ctrl Pts',(0.13155694143068,0.024465331227027,0.24));
#17570=CARTESIAN_POINT('Ctrl Pts',(0.134041462136676,0.0149150332268467,
0.24));
#17571=CARTESIAN_POINT('Ctrl Pts',(0.135496608205084,0.00520422800883078,
0.24));
#17572=CARTESIAN_POINT('Ctrl Pts',(0.136052940597398,0.00149158663520877,
0.24));
#17573=CARTESIAN_POINT('Ctrl Pts',(0.136458356591543,-0.00224482315054724,
0.24));
#17574=CARTESIAN_POINT('Ctrl Pts',(0.136708928272429,-0.00599574054845843,
0.24));
#17575=CARTESIAN_POINT('Ctrl Pts',(0.136894600108428,-0.00877514370161729,
0.24));
#17576=CARTESIAN_POINT('Ctrl Pts',(0.136994942037659,-0.0115613689854128,
0.24));
#17577=CARTESIAN_POINT('Ctrl Pts',(0.137008733057845,-0.0143405417274864,
0.24));
#17578=CARTESIAN_POINT('Ctrl Pts',(0.137045731231951,-0.0217964308202384,
0.24));
#17579=CARTESIAN_POINT('Ctrl Pts',(0.136462408227525,-0.0292204075226799,
0.24));
#17580=CARTESIAN_POINT('Ctrl Pts',(0.135240454646173,-0.0365388974416549,
0.24));
#17581=CARTESIAN_POINT('Ctrl Pts',(0.134058793448489,-0.0436160693529878,
0.24));
#17582=CARTESIAN_POINT('Ctrl Pts',(0.132280018312676,-0.050595007513092,
0.24));
#17583=CARTESIAN_POINT('Ctrl Pts',(0.129952822193542,-0.0574290655609092,
0.24));
#17584=CARTESIAN_POINT('Ctrl Pts',(0.128850070284018,-0.0606674134165377,
0.24));
#17585=CARTESIAN_POINT('Ctrl Pts',(0.127623182384127,-0.0638741644409745,
0.24));
#17586=CARTESIAN_POINT('Ctrl Pts',(0.126284110088584,-0.067028198101918,
0.24));
#17587=CARTESIAN_POINT('Ctrl Pts',(0.122654675969015,-0.0755769205431157,
0.24));
#17588=CARTESIAN_POINT('Ctrl Pts',(0.118195290975453,-0.0837663478860722,
0.24));
#17589=CARTESIAN_POINT('Ctrl Pts',(0.113014989178579,-0.0915013065162071,
0.24));
#17590=CARTESIAN_POINT('Ctrl Pts',(0.108985931714537,-0.0975172866704144,
0.24));
#17591=CARTESIAN_POINT('Ctrl Pts',(0.104519884911976,-0.103258562704539,
0.24));
#17592=CARTESIAN_POINT('Ctrl Pts',(0.0996546828651377,-0.108675969178894,
0.24));
#17593=CARTESIAN_POINT('Ctrl Pts',(0.0972822643803542,-0.11131765910988,
0.24));
#17594=CARTESIAN_POINT('Ctrl Pts',(0.09482095240722,-0.113875293456495,
0.24));
#17595=CARTESIAN_POINT('Ctrl Pts',(0.0922773332174137,-0.116342466058553,
0.24));
#17596=CARTESIAN_POINT('Ctrl Pts',(0.0868426048671788,-0.121613857680014,
0.24));
#17597=CARTESIAN_POINT('Ctrl Pts',(0.0810310485854155,-0.126474759557936,
0.24));
#17598=CARTESIAN_POINT('Ctrl Pts',(0.0748870600798396,-0.130870957562724,
0.24));
#17599=CARTESIAN_POINT('Ctrl Pts',(0.0715378781224404,-0.133267392228159,
0.24));
#17600=CARTESIAN_POINT('Ctrl Pts',(0.0680912231566627,-0.135524142754832,
0.24));
#17601=CARTESIAN_POINT('Ctrl Pts',(0.0645638484115253,-0.13762659390894,
0.24));
#17602=CARTESIAN_POINT('Ctrl Pts',(0.0598451535113139,-0.140439117742,0.24));
#17603=CARTESIAN_POINT('Ctrl Pts',(0.0549775790306604,-0.142978967531553,
0.24));
#17604=CARTESIAN_POINT('Ctrl Pts',(0.0499773507040556,-0.145225083935062,
0.24));
#17605=CARTESIAN_POINT('Ctrl Pts',(0.0466920976074369,-0.146700828718701,
0.24));
#17606=CARTESIAN_POINT('Ctrl Pts',(0.0433495270099635,-0.148049731670784,
0.24));
#17607=CARTESIAN_POINT('Ctrl Pts',(0.039956549802796,-0.149273502906639,
0.24));
#17608=CARTESIAN_POINT('Ctrl Pts',(-0.126296536029262,-6.10717992316628E-5,
0.159341967361942));
#17609=CARTESIAN_POINT('Ctrl Pts',(-0.12637083907321,-0.0163056929409037,
0.160361391877968));
#17610=CARTESIAN_POINT('Ctrl Pts',(-0.12344809088261,-0.0325245895549842,
0.161380816393994));
#17611=CARTESIAN_POINT('Ctrl Pts',(-0.117399968681154,-0.0474794518833934,
0.162400240910021));
#17612=CARTESIAN_POINT('Ctrl Pts',(-0.102053636235694,-0.0854254922118417,
0.164986899546353));
#17613=CARTESIAN_POINT('Ctrl Pts',(-0.0665853528586453,-0.115233359066084,
0.167573558182686));
#17614=CARTESIAN_POINT('Ctrl Pts',(-0.0265641275910804,-0.123819689910512,
0.170160216819019));
#17615=CARTESIAN_POINT('Ctrl Pts',(0.0134570976764845,-0.13240602075494,
0.172746875455351));
#17616=CARTESIAN_POINT('Ctrl Pts',(0.058031264834566,-0.119770815589554,
0.175333534091684));
#17617=CARTESIAN_POINT('Ctrl Pts',(0.0875924985281064,-0.0914586003428122,
0.177920192728017));
#17618=CARTESIAN_POINT('Ctrl Pts',(0.117153732221647,-0.0631463850960709,
0.180506851364349));
#17619=CARTESIAN_POINT('Ctrl Pts',(0.131702032450646,-0.0191571597679751,
0.183093510000682));
#17620=CARTESIAN_POINT('Ctrl Pts',(0.124851119980295,0.0211965060081854,
0.185680168637015));
#17621=CARTESIAN_POINT('Ctrl Pts',(0.118000207509943,0.0615501717843459,
0.188266827273347));
#17622=CARTESIAN_POINT('Ctrl Pts',(0.0897500823402403,0.0982682780085711,
0.19085348590968));
#17623=CARTESIAN_POINT('Ctrl Pts',(0.0525017161220023,0.115239608835997,
0.193440144546013));
#17624=CARTESIAN_POINT('Ctrl Pts',(0.0152533499037644,0.132210939663423,
0.196026803182345));
#17625=CARTESIAN_POINT('Ctrl Pts',(-0.030993257363009,0.129435495094051,
0.198613461818678));
#17626=CARTESIAN_POINT('Ctrl Pts',(-0.0659388717692058,0.108119484364762,
0.20120012045501));
#17627=CARTESIAN_POINT('Ctrl Pts',(-0.100884486175403,0.0868034736354726,
0.203786779091343));
#17628=CARTESIAN_POINT('Ctrl Pts',(-0.124529107721023,0.0469468967462671,
0.206373437727676));
#17629=CARTESIAN_POINT('Ctrl Pts',(-0.126492123469331,0.00606801008988057,
0.208960096364008));
#17630=CARTESIAN_POINT('Ctrl Pts',(-0.126588724127832,0.00405634646811867,
0.209087386696653));
#17631=CARTESIAN_POINT('Ctrl Pts',(-0.126632819376787,0.00204220716288977,
0.209214677029297));
#17632=CARTESIAN_POINT('Ctrl Pts',(-0.126625441102054,2.7778768752873E-5,
0.209341967361942));
#17633=CARTESIAN_POINT('Ctrl Pts',(-0.0398513841857245,-0.149064942821851,
0.24));
#17634=CARTESIAN_POINT('Ctrl Pts',(-0.0883048112969314,-0.136111285829332,
0.237413341363667));
#17635=CARTESIAN_POINT('Ctrl Pts',(-0.170871437255804,-0.0596187094618861,
0.232240024091002));
#17636=CARTESIAN_POINT('Ctrl Pts',(-0.145169204726118,0.108307533342445,
0.224480048182004));
#17637=CARTESIAN_POINT('Ctrl Pts',(0.00818767200092134,0.180778621679153,
0.216720072273006));
#17638=CARTESIAN_POINT('Ctrl Pts',(0.154249898498561,0.0947283641859207,
0.208960096364008));
#17639=CARTESIAN_POINT('Ctrl Pts',(0.164950538597243,-0.0745810526211722,
0.201200120455011));
#17640=CARTESIAN_POINT('Ctrl Pts',(0.0308106631569891,-0.178364693496558,
0.193440144546012));
#17641=CARTESIAN_POINT('Ctrl Pts',(-0.13036283225522,-0.125587074703769,
0.185680168637015));
#17642=CARTESIAN_POINT('Ctrl Pts',(-0.17709781441264,0.03745832727601,0.177920192728017));
#17643=CARTESIAN_POINT('Ctrl Pts',(-0.0683530255288039,0.167611467503216,
0.170160216819019));
#17644=CARTESIAN_POINT('Ctrl Pts',(0.100397202365132,0.150621028353064,
0.162400240910021));
#17645=CARTESIAN_POINT('Ctrl Pts',(0.18100910679194,0.00139719974911195,
0.154640265001023));
#17646=CARTESIAN_POINT('Ctrl Pts',(0.102711092909207,-0.149052183789333,
0.146880289092025));
#17647=CARTESIAN_POINT('Ctrl Pts',(-0.0657574679958034,-0.168648048308422,
0.139120313183027));
#17648=CARTESIAN_POINT('Ctrl Pts',(-0.176497206835689,-0.0401861834345609,
0.131360337274029));
#17649=CARTESIAN_POINT('Ctrl Pts',(-0.132288575936487,0.123555290563421,
0.123600361365031));
#17650=CARTESIAN_POINT('Ctrl Pts',(0.0280571680938306,0.178826694862324,
0.115840385456033));
#17651=CARTESIAN_POINT('Ctrl Pts',(0.163771354656592,0.0771047007047774,
0.108080409547035));
#17652=CARTESIAN_POINT('Ctrl Pts',(0.155709331479018,-0.0923080778690166,
0.100320433638038));
#17653=CARTESIAN_POINT('Ctrl Pts',(0.0109489686262093,-0.180682908560435,
0.0925604577290397));
#17654=CARTESIAN_POINT('Ctrl Pts',(-0.143423754439364,-0.110434756566834,
0.0848004818200417));
#17655=CARTESIAN_POINT('Ctrl Pts',(-0.17188331593326,0.0567648465404429,
0.0770405059110439));
#17656=CARTESIAN_POINT('Ctrl Pts',(-0.0494457976037486,0.174130301808973,
0.0692805300020459));
#17657=CARTESIAN_POINT('Ctrl Pts',(0.11640175885633,0.13862511662766,0.061520554093048));
#17658=CARTESIAN_POINT('Ctrl Pts',(0.18005704388064,-0.0185795878987759,
0.0537605781840501));
#17659=CARTESIAN_POINT('Ctrl Pts',(0.0856431484406112,-0.159474177462153,
0.0460006022750521));
#17660=CARTESIAN_POINT('Ctrl Pts',(-0.0839657292871194,-0.160363143120653,
0.0382406263660544));
#17661=CARTESIAN_POINT('Ctrl Pts',(-0.179844832231877,-0.0204718628801216,
0.0304806504570563));
#17662=CARTESIAN_POINT('Ctrl Pts',(-0.117866479118068,0.137399078213474,
0.0227206745480585));
#17663=CARTESIAN_POINT('Ctrl Pts',(0.0476444145610997,0.174632482457551,
0.0149606986390605));
#17664=CARTESIAN_POINT('Ctrl Pts',(0.171219786572432,0.0585809927800803,
0.00720072273006264));
#17665=CARTESIAN_POINT('Ctrl Pts',(0.144688050375066,-0.108949473877577,
-0.000559253178935319));
#17666=CARTESIAN_POINT('Ctrl Pts',(-0.0092814439579932,-0.180735423716049,
-0.00831922908793317));
#17667=CARTESIAN_POINT('Ctrl Pts',(-0.105867686800049,-0.122947365648507,
-0.0134925463605985));
#17668=CARTESIAN_POINT('Ctrl Pts',(-0.131895903200816,-0.0800747195988904,
-0.0160792049969312));
#17669=CARTESIAN_POINT('Ctrl Pts',(-0.0374537582415196,-0.140096572423086,
0.245359734998977));
#17670=CARTESIAN_POINT('Ctrl Pts',(-0.0829920245295529,-0.127922261611689,
0.242773076362644));
#17671=CARTESIAN_POINT('Ctrl Pts',(-0.160591096949962,-0.0560317985556137,
0.237599759089979));
#17672=CARTESIAN_POINT('Ctrl Pts',(-0.13643521822445,0.101791299158848,
0.229839783180981));
#17673=CARTESIAN_POINT('Ctrl Pts',(0.00769506740980954,0.1699022237233,
0.222079807271983));
#17674=CARTESIAN_POINT('Ctrl Pts',(0.144969579481095,0.0890291096113304,
0.214319831362985));
#17675=CARTESIAN_POINT('Ctrl Pts',(0.155026424317845,-0.0700939445729984,
0.206559855453987));
#17676=CARTESIAN_POINT('Ctrl Pts',(0.0289569648011409,-0.167633527556011,
0.19879987954499));
#17677=CARTESIAN_POINT('Ctrl Pts',(-0.122519659046519,-0.118031231043151,
0.191039903635991));
#17678=CARTESIAN_POINT('Ctrl Pts',(-0.166442869216287,0.0352046776440443,
0.183279927726994));
#17679=CARTESIAN_POINT('Ctrl Pts',(-0.064240621638164,0.157527260611955,
0.175519951817996));
#17680=CARTESIAN_POINT('Ctrl Pts',(0.0943568867767351,0.141559037340679,
0.167759975908998));
#17681=CARTESIAN_POINT('Ctrl Pts',(0.170118841887737,0.00131313836865665,
0.16));
#17682=CARTESIAN_POINT('Ctrl Pts',(0.0965315639882279,-0.140084581027326,
0.152240024091002));
#17683=CARTESIAN_POINT('Ctrl Pts',(-0.0618012237018238,-0.158501476380598,
0.144480048182004));
#17684=CARTESIAN_POINT('Ctrl Pts',(-0.165878396703103,-0.0377684145673052,
0.136720072273006));
#17685=CARTESIAN_POINT('Ctrl Pts',(-0.124329541933827,0.116121687534276,
0.128960096364008));
#17686=CARTESIAN_POINT('Ctrl Pts',(0.0263691315170036,0.168067732987372,
0.12120012045501));
#17687=CARTESIAN_POINT('Ctrl Pts',(0.153918185014798,0.0724657594331675,
0.113440144546012));
#17688=CARTESIAN_POINT('Ctrl Pts',(0.146341206869619,-0.0867544378416841,
0.105680168637015));
#17689=CARTESIAN_POINT('Ctrl Pts',(0.0102902328814698,-0.169812269106107,
0.0979201927280167));
#17690=CARTESIAN_POINT('Ctrl Pts',(-0.134794781526993,-0.103790539737311,
0.0901602168190187));
#17691=CARTESIAN_POINT('Ctrl Pts',(-0.161542096774173,0.0533496359633175,
0.0824002409100209));
#17692=CARTESIAN_POINT('Ctrl Pts',(-0.0464709316213242,0.163653894581969,
0.074640265001023));
#17693=CARTESIAN_POINT('Ctrl Pts',(0.109398542213106,0.130284849835523,
0.066880289092025));
#17694=CARTESIAN_POINT('Ctrl Pts',(0.16922405906302,-0.0174617621848401,
0.0591203131830272));
#17695=CARTESIAN_POINT('Ctrl Pts',(0.0804904984426183,-0.149879543972585,
0.0513603372740291));
#17696=CARTESIAN_POINT('Ctrl Pts',(-0.0789139998409189,-0.150715025739123,
0.0436003613650314));
#17697=CARTESIAN_POINT('Ctrl Pts',(-0.169024614954586,-0.0192401899891918,
0.0358403854560333));
#17698=CARTESIAN_POINT('Ctrl Pts',(-0.110775138777956,0.12913257502003,
0.0280804095470356));
#17699=CARTESIAN_POINT('Ctrl Pts',(0.0447779273164969,0.164125861942445,
0.0203204336380375));
#17700=CARTESIAN_POINT('Ctrl Pts',(0.16091848811479,0.0550565152494576,
0.0125604577290397));
#17701=CARTESIAN_POINT('Ctrl Pts',(0.135983012131502,-0.10239461786658,
0.00480048182004171));
#17702=CARTESIAN_POINT('Ctrl Pts',(-0.00872303347143,-0.169861624730324,
-0.00295949408895612));
#17703=CARTESIAN_POINT('Ctrl Pts',(-0.0994982439886826,-0.115550337924785,
-0.00813281136162148));
#17704=CARTESIAN_POINT('Ctrl Pts',(-0.123960494032221,-0.0752570895690155,
-0.0107194699979541));
#17705=CARTESIAN_POINT('Ctrl Pts',(-0.0350561322973148,-0.13112820202432,
0.250719469997954));
#17706=CARTESIAN_POINT('Ctrl Pts',(-0.0776792377621743,-0.119733237394047,
0.248132811361621));
#17707=CARTESIAN_POINT('Ctrl Pts',(-0.150310756644121,-0.0524448876493412,
0.242959494088956));
#17708=CARTESIAN_POINT('Ctrl Pts',(-0.127701231722781,0.0952750649752511,
0.235199518179958));
#17709=CARTESIAN_POINT('Ctrl Pts',(0.00720246281869772,0.159025825767447,
0.22743954227096));
#17710=CARTESIAN_POINT('Ctrl Pts',(0.135689260463629,0.08332985503674,0.219679566361962));
#17711=CARTESIAN_POINT('Ctrl Pts',(0.145102310038447,-0.0656068365248246,
0.211919590452964));
#17712=CARTESIAN_POINT('Ctrl Pts',(0.0271032664452926,-0.156902361615465,
0.204159614543967));
#17713=CARTESIAN_POINT('Ctrl Pts',(-0.114676485837817,-0.110475387382534,
0.196399638634969));
#17714=CARTESIAN_POINT('Ctrl Pts',(-0.155787924019933,0.0329510280120788,
0.188639662725971));
#17715=CARTESIAN_POINT('Ctrl Pts',(-0.0601282177475243,0.147443053720694,
0.180879686816973));
#17716=CARTESIAN_POINT('Ctrl Pts',(0.0883165711883383,0.132497046328295,
0.173119710907975));
#17717=CARTESIAN_POINT('Ctrl Pts',(0.159228576983534,0.00122907698820117,
0.165359734998977));
#17718=CARTESIAN_POINT('Ctrl Pts',(0.0903520350672485,-0.131116978265319,
0.157599759089979));
#17719=CARTESIAN_POINT('Ctrl Pts',(-0.0578449794078444,-0.148354904452775,
0.149839783180981));
#17720=CARTESIAN_POINT('Ctrl Pts',(-0.155259586570517,-0.0353506457000499,
0.142079807271983));
#17721=CARTESIAN_POINT('Ctrl Pts',(-0.116370507931168,0.108688084505131,
0.134319831362985));
#17722=CARTESIAN_POINT('Ctrl Pts',(0.0246810949401768,0.157308771112418,
0.126559855453988));
#17723=CARTESIAN_POINT('Ctrl Pts',(0.144065015373005,0.0678268181615582,
0.118799879544989));
#17724=CARTESIAN_POINT('Ctrl Pts',(0.13697308226022,-0.0812007978143519,
0.111039903635992));
#17725=CARTESIAN_POINT('Ctrl Pts',(0.00963149713673027,-0.15894162965178,
0.103279927726994));
#17726=CARTESIAN_POINT('Ctrl Pts',(-0.126165808614623,-0.0971463229077874,
0.0955199518179957));
#17727=CARTESIAN_POINT('Ctrl Pts',(-0.151200877615086,0.0499344253861922,
0.087759975908998));
#17728=CARTESIAN_POINT('Ctrl Pts',(-0.0434960656388994,0.153177487354966,
0.08));
#17729=CARTESIAN_POINT('Ctrl Pts',(0.102395325569881,0.121944583043386,
0.072240024091002));
#17730=CARTESIAN_POINT('Ctrl Pts',(0.158391074245402,-0.0163439364709043,
0.0644800481820042));
#17731=CARTESIAN_POINT('Ctrl Pts',(0.0753378484446251,-0.140284910483017,
0.0567200722730062));
#17732=CARTESIAN_POINT('Ctrl Pts',(-0.0738622703947183,-0.141066908357593,
0.0489600963640083));
#17733=CARTESIAN_POINT('Ctrl Pts',(-0.158204397677296,-0.018008517098262,
0.0412001204550104));
#17734=CARTESIAN_POINT('Ctrl Pts',(-0.103683798437843,0.120866071826586,
0.0334401445460125));
#17735=CARTESIAN_POINT('Ctrl Pts',(0.0419114400718942,0.153619241427338,
0.0256801686370146));
#17736=CARTESIAN_POINT('Ctrl Pts',(0.150617189657149,0.051532037718835,
0.0179201927280167));
#17737=CARTESIAN_POINT('Ctrl Pts',(0.127277973887939,-0.0958397618555833,
0.0101602168190187));
#17738=CARTESIAN_POINT('Ctrl Pts',(-0.00816462298486686,-0.1589878257446,
0.00240024091002091));
#17739=CARTESIAN_POINT('Ctrl Pts',(-0.0931288011773165,-0.108153310201063,
-0.00277307636264444));
#17740=CARTESIAN_POINT('Ctrl Pts',(-0.116025084863626,-0.0704394595391406,
-0.00535973499897709));
#17741=CARTESIAN_POINT('Ctrl Pts',(-0.0326585063531099,-0.122159831625555,
0.256079204996931));
#17742=CARTESIAN_POINT('Ctrl Pts',(-0.0723664509947957,-0.111544213176404,
0.253492546360598));
#17743=CARTESIAN_POINT('Ctrl Pts',(-0.140030416338279,-0.0488579767430688,
0.248319229087933));
#17744=CARTESIAN_POINT('Ctrl Pts',(-0.118967245221113,0.0887588307916541,
0.240559253178936));
#17745=CARTESIAN_POINT('Ctrl Pts',(0.00670985822758596,0.148149427811594,
0.232799277269937));
#17746=CARTESIAN_POINT('Ctrl Pts',(0.126408941446163,0.0776306004621497,
0.225039301360939));
#17747=CARTESIAN_POINT('Ctrl Pts',(0.13517819575905,-0.0611197284766509,
0.217279325451942));
#17748=CARTESIAN_POINT('Ctrl Pts',(0.0252495680894444,-0.146171195674918,
0.209519349542944));
#17749=CARTESIAN_POINT('Ctrl Pts',(-0.106833312629116,-0.102919543721916,
0.201759373633946));
#17750=CARTESIAN_POINT('Ctrl Pts',(-0.14513297882358,0.0306973783801131,
0.193999397724948));
#17751=CARTESIAN_POINT('Ctrl Pts',(-0.0560158138568844,0.137358846829434,
0.18623942181595));
#17752=CARTESIAN_POINT('Ctrl Pts',(0.0822762555999414,0.12343505531591,
0.178479445906952));
#17753=CARTESIAN_POINT('Ctrl Pts',(0.148338312079331,0.00114501560774606,
0.170719469997954));
#17754=CARTESIAN_POINT('Ctrl Pts',(0.0841725061462688,-0.122149375503312,
0.162959494088956));
#17755=CARTESIAN_POINT('Ctrl Pts',(-0.0538887351138648,-0.138208332524951,
0.155199518179959));
#17756=CARTESIAN_POINT('Ctrl Pts',(-0.144640776437932,-0.0329328768327946,
0.14743954227096));
#17757=CARTESIAN_POINT('Ctrl Pts',(-0.108411473928508,0.101254481475986,
0.139679566361963));
#17758=CARTESIAN_POINT('Ctrl Pts',(0.0229930583633497,0.146549809237466,
0.131919590452964));
#17759=CARTESIAN_POINT('Ctrl Pts',(0.134211845731212,0.0631878768899486,
0.124159614543967));
#17760=CARTESIAN_POINT('Ctrl Pts',(0.127604957650822,-0.0756471577870196,
0.116399638634969));
#17761=CARTESIAN_POINT('Ctrl Pts',(0.00897276139199077,-0.148070990197453,
0.108639662725971));
#17762=CARTESIAN_POINT('Ctrl Pts',(-0.117536835702253,-0.0905021060782641,
0.100879686816973));
#17763=CARTESIAN_POINT('Ctrl Pts',(-0.140859658455999,0.0465192148090667,
0.0931197109079749));
#17764=CARTESIAN_POINT('Ctrl Pts',(-0.0405211996564747,0.142701080127962,
0.0853597349989771));
#17765=CARTESIAN_POINT('Ctrl Pts',(0.0953921089266558,0.113604316251249,
0.077599759089979));
#17766=CARTESIAN_POINT('Ctrl Pts',(0.147558089427783,-0.0152261107569683,
0.0698397831809813));
#17767=CARTESIAN_POINT('Ctrl Pts',(0.070185198446632,-0.130690276993449,
0.0620798072719832));
#17768=CARTESIAN_POINT('Ctrl Pts',(-0.0688105409485176,-0.131418790976063,
0.0543198313629854));
#17769=CARTESIAN_POINT('Ctrl Pts',(-0.147384180400005,-0.0167768442073323,
0.0465598554539874));
#17770=CARTESIAN_POINT('Ctrl Pts',(-0.0965924580977301,0.112599568633142,
0.0387998795449896));
#17771=CARTESIAN_POINT('Ctrl Pts',(0.0390449528272914,0.143112620912232,
0.0310399036359916));
#17772=CARTESIAN_POINT('Ctrl Pts',(0.140315891199508,0.0480075601882123,
0.0232799277269937));
#17773=CARTESIAN_POINT('Ctrl Pts',(0.118572935644375,-0.0892849058445864,
0.0155199518179958));
#17774=CARTESIAN_POINT('Ctrl Pts',(-0.00760621249830358,-0.148114026758875,
0.00775997590899793));
#17775=CARTESIAN_POINT('Ctrl Pts',(-0.0867593583659504,-0.100756282477341,
0.00258665863633259));
#17776=CARTESIAN_POINT('Ctrl Pts',(-0.108089675695031,-0.0656218295092657,
-5.55111512312578E-17));
#17777=CARTESIAN_POINT('Ctrl Pts',(-0.108089675695031,-0.0656218295092657,
-5.55111512312578E-17));
#17778=CARTESIAN_POINT('Ctrl Pts',(-0.104219465379748,-0.0739058869203245,
-4.02841154597017E-17));
#17779=CARTESIAN_POINT('Ctrl Pts',(-0.0994141168358061,-0.0816768736924768,
-5.16144647363644E-17));
#17780=CARTESIAN_POINT('Ctrl Pts',(-0.0938412360364922,-0.088871564406415,
-3.81639164714898E-17));
#17781=CARTESIAN_POINT('Ctrl Pts',(-0.0894001862863345,-0.094605040600905,
-2.74451237748006E-17));
#17782=CARTESIAN_POINT('Ctrl Pts',(-0.0844703330957707,-0.0999727304469881,
3.12377098840079E-17));
#17783=CARTESIAN_POINT('Ctrl Pts',(-0.0791158513129458,-0.104935071387697,
-1.21430643318376E-17));
#17784=CARTESIAN_POINT('Ctrl Pts',(-0.0766900604813501,-0.107183206995485,
-3.17962611543325E-17));
#17785=CARTESIAN_POINT('Ctrl Pts',(-0.0741829996358932,-0.109342173006691,
4.83248416902999E-17));
#17786=CARTESIAN_POINT('Ctrl Pts',(-0.0716059924168524,-0.111405381598006,
5.3776427755281E-17));
#17787=CARTESIAN_POINT('Ctrl Pts',(-0.0639212992135713,-0.117557915794061,
7.00331794132204E-17));
#17788=CARTESIAN_POINT('Ctrl Pts',(-0.0556061968393146,-0.12287204611112,
-5.69073736333764E-18));
#17789=CARTESIAN_POINT('Ctrl Pts',(-0.0468203466856493,-0.127256781127915,
5.55111512312578E-17));
#17790=CARTESIAN_POINT('Ctrl Pts',(-0.0434613267337519,-0.12893315986732,
7.89099528597243E-17));
#17791=CARTESIAN_POINT('Ctrl Pts',(-0.0400330653128497,-0.130473352587733,
3.97002991909352E-17));
#17792=CARTESIAN_POINT('Ctrl Pts',(-0.0365431560942257,-0.131870761756357,
6.59194920871187E-17));
#17793=CARTESIAN_POINT('Ctrl Pts',(-0.0339571636773035,-0.13290622981212,
8.5347686277821E-17));
#17794=CARTESIAN_POINT('Ctrl Pts',(-0.0313383144727484,-0.133862652235137,
-2.74403076010104E-17));
#17795=CARTESIAN_POINT('Ctrl Pts',(-0.0286994266230122,-0.134734580282325,
-2.42861286636753E-17));
#17796=CARTESIAN_POINT('Ctrl Pts',(-0.0216199050576346,-0.137073760181214,
-1.58242011095522E-17));
#17797=CARTESIAN_POINT('Ctrl Pts',(-0.0143790427459088,-0.138813119073991,
5.80198461902811E-17));
#17798=CARTESIAN_POINT('Ctrl Pts',(-0.0070411538297537,-0.139912507657099,
6.93889390390723E-17));
#17799=CARTESIAN_POINT('Ctrl Pts',(5.47883476400097E-5,-0.140975646920361,
8.02325614020808E-17));
#17800=CARTESIAN_POINT('Ctrl Pts',(0.00724182591717642,-0.141440539972256,
1.32011341321413E-16));
#17801=CARTESIAN_POINT('Ctrl Pts',(0.0144605478337719,-0.141339082434075,
1.61329283265843E-16));
#17802=CARTESIAN_POINT('Ctrl Pts',(0.0178811722145177,-0.141291006315792,
1.75221724083914E-16));
#17803=CARTESIAN_POINT('Ctrl Pts',(0.021310106848269,-0.141115105569205,
1.85534911235541E-16));
#17804=CARTESIAN_POINT('Ctrl Pts',(0.0247235715439624,-0.140816220288761,
1.71737624121704E-16));
#17805=CARTESIAN_POINT('Ctrl Pts',(0.0339754553361668,-0.140006119078294,
1.34341339582434E-16));
#17806=CARTESIAN_POINT('Ctrl Pts',(0.0431421008898472,-0.138295657968001,
8.04496487960062E-17));
#17807=CARTESIAN_POINT('Ctrl Pts',(0.0520992976556894,-0.135759125106636,
3.20923843055709E-17));
#17808=CARTESIAN_POINT('Ctrl Pts',(0.0590658916121619,-0.13378629867842,
-5.518202506064E-18));
#17809=CARTESIAN_POINT('Ctrl Pts',(0.0659062642374416,-0.131312982137409,
7.87850579480063E-17));
#17810=CARTESIAN_POINT('Ctrl Pts',(0.0725619642951071,-0.128359965266718,
7.63278329429795E-17));
#17811=CARTESIAN_POINT('Ctrl Pts',(0.0758074813473741,-0.126919986522721,
7.51296170399226E-17));
#17812=CARTESIAN_POINT('Ctrl Pts',(0.0790005264283722,-0.125369490597537,
8.38688896655138E-17));
#17813=CARTESIAN_POINT('Ctrl Pts',(0.0821329715644795,-0.123712761836801,
7.24247051220317E-17));
#17814=CARTESIAN_POINT('Ctrl Pts',(0.0888257654942848,-0.120172989003949,
4.79730178566093E-17));
#17815=CARTESIAN_POINT('Ctrl Pts',(0.0952446087626691,-0.116147988031934,
8.96774285244103E-17));
#17816=CARTESIAN_POINT('Ctrl Pts',(0.101324221742587,-0.111663228753314,
8.28330459778925E-17));
#17817=CARTESIAN_POINT('Ctrl Pts',(0.104638321741973,-0.109218510516871,
7.91020571356516E-17));
#17818=CARTESIAN_POINT('Ctrl Pts',(0.107849695272814,-0.106637925639498,
3.17151869302413E-17));
#17819=CARTESIAN_POINT('Ctrl Pts',(0.110939265073957,-0.10393289123317,
1.53956708492942E-17));
#17820=CARTESIAN_POINT('Ctrl Pts',(0.115072333360666,-0.100314234708527,
-6.43574216607592E-18));
#17821=CARTESIAN_POINT('Ctrl Pts',(0.118992075260627,-0.0964697210975667,
5.54296751400654E-17));
#17822=CARTESIAN_POINT('Ctrl Pts',(0.122673447199167,-0.0924082746861152,
3.52365706057789E-17));
#17823=CARTESIAN_POINT('Ctrl Pts',(0.125092164655522,-0.0897398425098966,
2.31620156359627E-17));
#17824=CARTESIAN_POINT('Ctrl Pts',(0.127407959881093,-0.0869777021544565,
-4.01489640485901E-17));
#17825=CARTESIAN_POINT('Ctrl Pts',(0.129620323775263,-0.0841289546921697,
-3.98986399474666E-17));
#17826=CARTESIAN_POINT('Ctrl Pts',(-0.126471935391749,0.000101176582396995,
0.195658032638058));
#17827=CARTESIAN_POINT('Ctrl Pts',(-0.126547267107008,0.00888033934128026,
0.195105154333688));
#17828=CARTESIAN_POINT('Ctrl Pts',(-0.125707148272093,0.0176451944231377,
0.194552276029318));
#17829=CARTESIAN_POINT('Ctrl Pts',(-0.12389684029672,0.0262048027713284,
0.193999397724948));
#17830=CARTESIAN_POINT('Ctrl Pts',(-0.115427257168015,0.0662512011965534,
0.191412739088615));
#17831=CARTESIAN_POINT('Ctrl Pts',(-0.0857215355124495,0.101805024012994,
0.188826080452282));
#17832=CARTESIAN_POINT('Ctrl Pts',(-0.0478199964418627,0.117261303502293,
0.18623942181595));
#17833=CARTESIAN_POINT('Ctrl Pts',(-0.0099184573712758,0.132717582991593,
0.183652763179617));
#17834=CARTESIAN_POINT('Ctrl Pts',(0.0361788991143328,0.128076319153751,
0.181066104543285));
#17835=CARTESIAN_POINT('Ctrl Pts',(0.070237920103702,0.105374013950137,
0.178479445906952));
#17836=CARTESIAN_POINT('Ctrl Pts',(0.104296941093071,0.0826717087465222,
0.175892787270619));
#17837=CARTESIAN_POINT('Ctrl Pts',(0.126317626586201,0.0419083621771342,
0.173306128634287));
#17838=CARTESIAN_POINT('Ctrl Pts',(0.126633668343922,0.000977623707263797,
0.170719469997954));
#17839=CARTESIAN_POINT('Ctrl Pts',(0.126949710101644,-0.0399531147626067,
0.168132811361621));
#17840=CARTESIAN_POINT('Ctrl Pts',(0.105561108123956,-0.08105124513296,
0.165546152725289));
#17841=CARTESIAN_POINT('Ctrl Pts',(0.0718566002584231,-0.104276803155076,
0.162959494088956));
#17842=CARTESIAN_POINT('Ctrl Pts',(0.0381520923928904,-0.127502361177192,
0.160372835452623));
#17843=CARTESIAN_POINT('Ctrl Pts',(-0.00786832136048696,-0.132855346851071,
0.157786176816291));
#17844=CARTESIAN_POINT('Ctrl Pts',(-0.0460038684578537,-0.117985930405985,
0.155199518179958));
#17845=CARTESIAN_POINT('Ctrl Pts',(-0.0841394155552204,-0.103116513960899,
0.152612859543626));
#17846=CARTESIAN_POINT('Ctrl Pts',(-0.114390095996576,-0.0680246953968468,
0.150026200907293));
#17847=CARTESIAN_POINT('Ctrl Pts',(-0.12347721913235,-0.0281142263966907,
0.14743954227096));
#17848=CARTESIAN_POINT('Ctrl Pts',(-0.125563410841138,-0.018951712774069,
0.14684570572666));
#17849=CARTESIAN_POINT('Ctrl Pts',(-0.126534167537385,-0.00953522996602069,
0.146251869182359));
#17850=CARTESIAN_POINT('Ctrl Pts',(-0.126453631260982,-0.000102348163238207,
0.145658032638058));
#17851=CARTESIAN_POINT('Ctrl Pts',(-0.0398513841857245,-0.149064942821851,
0.24));
#17852=CARTESIAN_POINT('Ctrl Pts',(-0.0498806325786677,-0.145400296738327,
0.24));
#17853=CARTESIAN_POINT('Ctrl Pts',(-0.0594363948008725,-0.140639648297949,
0.24));
#17854=CARTESIAN_POINT('Ctrl Pts',(-0.0684062055177017,-0.134931499399492,
0.24));
#17855=CARTESIAN_POINT('Ctrl Pts',(-0.0735915624001909,-0.131631676235849,
0.24));
#17856=CARTESIAN_POINT('Ctrl Pts',(-0.0785806353345173,-0.128014298080738,
0.24));
#17857=CARTESIAN_POINT('Ctrl Pts',(-0.0833462611484583,-0.124102693747304,
0.24));
#17858=CARTESIAN_POINT('Ctrl Pts',(-0.0858656342542594,-0.122034803580736,
0.24));
#17859=CARTESIAN_POINT('Ctrl Pts',(-0.0883241156266364,-0.11988309220465,
0.24));
#17860=CARTESIAN_POINT('Ctrl Pts',(-0.0907117892851122,-0.117655751751618,
0.24));
#17861=CARTESIAN_POINT('Ctrl Pts',(-0.0983819858496404,-0.110500611839494,
0.24));
#17862=CARTESIAN_POINT('Ctrl Pts',(-0.105284458416918,-0.102606966330569,
0.24));
#17863=CARTESIAN_POINT('Ctrl Pts',(-0.111294422020379,-0.0941015332659665,
0.24));
#17864=CARTESIAN_POINT('Ctrl Pts',(-0.114410577497229,-0.0896914812962706,
0.24));
#17865=CARTESIAN_POINT('Ctrl Pts',(-0.117286101138547,-0.0851164738413172,
0.24));
#17866=CARTESIAN_POINT('Ctrl Pts',(-0.119898298320422,-0.0803922539627851,
0.24));
#17867=CARTESIAN_POINT('Ctrl Pts',(-0.1222721977331,-0.0760990011896685,
0.24));
#17868=CARTESIAN_POINT('Ctrl Pts',(-0.124430744329062,-0.0716759619599862,
0.24));
#17869=CARTESIAN_POINT('Ctrl Pts',(-0.126341093034125,-0.0671690272221462,
0.24));
#17870=CARTESIAN_POINT('Ctrl Pts',(-0.129206708925078,-0.060408406100978,
0.24));
#17871=CARTESIAN_POINT('Ctrl Pts',(-0.131522065955468,-0.0534490321795157,
0.24));
#17872=CARTESIAN_POINT('Ctrl Pts',(-0.133233091500091,-0.0463330844490581,
0.24));
#17873=CARTESIAN_POINT('Ctrl Pts',(-0.135004134506116,-0.0389675313754268,
0.24));
#17874=CARTESIAN_POINT('Ctrl Pts',(-0.136127599829873,-0.0314337185245799,
0.24));
#17875=CARTESIAN_POINT('Ctrl Pts',(-0.136615064298196,-0.0238138180582873,
0.24));
#17876=CARTESIAN_POINT('Ctrl Pts',(-0.136813484749433,-0.0207121682209076,
0.24));
#17877=CARTESIAN_POINT('Ctrl Pts',(-0.136906013213758,-0.0175970392000076,
0.24));
#17878=CARTESIAN_POINT('Ctrl Pts',(-0.136893785357156,-0.0144871321155608,
0.24));
#17879=CARTESIAN_POINT('Ctrl Pts',(-0.136861203984761,-0.00620072149302863,
0.24));
#17880=CARTESIAN_POINT('Ctrl Pts',(-0.136088646936857,0.00207357465703332,
0.24));
#17881=CARTESIAN_POINT('Ctrl Pts',(-0.134599584032292,0.0102285531249486,
0.24));
#17882=CARTESIAN_POINT('Ctrl Pts',(-0.133676409755049,0.0152843948425598,
0.24));
#17883=CARTESIAN_POINT('Ctrl Pts',(-0.132477333465274,0.0202942984003417,
0.24));
#17884=CARTESIAN_POINT('Ctrl Pts',(-0.131003622030167,0.0252303138624672,
0.24));
#17885=CARTESIAN_POINT('Ctrl Pts',(-0.129740734874544,0.029460199292259,
0.24));
#17886=CARTESIAN_POINT('Ctrl Pts',(-0.128274507607502,0.0336384499732856,
0.24));
#17887=CARTESIAN_POINT('Ctrl Pts',(-0.126614574688298,0.0377237273426867,
0.24));
#17888=CARTESIAN_POINT('Ctrl Pts',(-0.124573382985647,0.042747324485064,
0.24));
#17889=CARTESIAN_POINT('Ctrl Pts',(-0.122237651925267,0.0476379767326878,
0.24));
#17890=CARTESIAN_POINT('Ctrl Pts',(-0.119609691052418,0.0523617558795304,
0.24));
#17891=CARTESIAN_POINT('Ctrl Pts',(-0.117006563775536,0.0570408964535612,
0.24));
#17892=CARTESIAN_POINT('Ctrl Pts',(-0.114113358229268,0.0615597689541448,
0.24));
#17893=CARTESIAN_POINT('Ctrl Pts',(-0.110947628485839,0.0658586917144141,
0.24));
#17894=CARTESIAN_POINT('Ctrl Pts',(-0.108265305855902,0.0695011687224882,
0.24));
#17895=CARTESIAN_POINT('Ctrl Pts',(-0.105385772272888,0.0729892759232728,
0.24));
#17896=CARTESIAN_POINT('Ctrl Pts',(-0.102309360287629,0.0763011815833395,
0.24));
#17897=CARTESIAN_POINT('Ctrl Pts',(-0.100282916666232,0.0784827457339379,
0.24));
#17898=CARTESIAN_POINT('Ctrl Pts',(-0.0981709975111385,0.0805877996091198,
0.24));
#17899=CARTESIAN_POINT('Ctrl Pts',(-0.0959791030802606,0.0826138105732947,
0.24));
#17900=CARTESIAN_POINT('Origin',(0.,0.,0.24));
#17901=CARTESIAN_POINT('',(0.158771324027147,-0.275,0.24));
#17902=CARTESIAN_POINT('',(0.317542648054294,0.,0.24));
#17903=CARTESIAN_POINT('',(0.158771324027147,-0.275,0.24));
#17904=CARTESIAN_POINT('',(0.158771324027147,0.275,0.24));
#17905=CARTESIAN_POINT('',(0.317542648054294,0.,0.24));
#17906=CARTESIAN_POINT('',(-0.158771324027147,0.275,0.24));
#17907=CARTESIAN_POINT('',(0.158771324027147,0.275,0.24));
#17908=CARTESIAN_POINT('',(-0.317542648054294,5.55111512312578E-17,0.24));
#17909=CARTESIAN_POINT('',(-0.158771324027147,0.275,0.24));
#17910=CARTESIAN_POINT('',(-0.158771324027147,-0.275,0.24));
#17911=CARTESIAN_POINT('',(-0.317542648054294,3.88877587532466E-17,0.24));
#17912=CARTESIAN_POINT('',(-0.158771324027147,-0.275,0.24));
#17913=CARTESIAN_POINT('Origin',(0.,0.,0.12));
#17914=CARTESIAN_POINT('Origin',(-0.158771324027147,-0.275,0.));
#17915=CARTESIAN_POINT('',(-0.158771324027147,-0.275,0.));
#17916=CARTESIAN_POINT('',(0.158771324027147,-0.275,0.));
#17917=CARTESIAN_POINT('',(-0.158771324027147,-0.275,0.));
#17918=CARTESIAN_POINT('',(0.158771324027147,-0.275,0.));
#17919=CARTESIAN_POINT('',(-0.158771324027147,-0.275,0.));
#17920=CARTESIAN_POINT('Origin',(-0.317542648054294,3.88877587532466E-17,
0.));
#17921=CARTESIAN_POINT('',(-0.317542648054294,3.88877587532466E-17,0.));
#17922=CARTESIAN_POINT('',(-0.317542648054294,3.88877587532466E-17,0.));
#17923=CARTESIAN_POINT('',(-0.317542648054294,3.88877587532466E-17,0.));
#17924=CARTESIAN_POINT('Origin',(-0.158771324027147,0.275,0.));
#17925=CARTESIAN_POINT('',(-0.158771324027147,0.275,0.));
#17926=CARTESIAN_POINT('',(-0.158771324027147,0.275,0.));
#17927=CARTESIAN_POINT('',(-0.158771324027147,0.275,0.));
#17928=CARTESIAN_POINT('Origin',(0.158771324027147,0.275,0.));
#17929=CARTESIAN_POINT('',(0.158771324027147,0.275,0.));
#17930=CARTESIAN_POINT('',(0.158771324027147,0.275,0.));
#17931=CARTESIAN_POINT('',(0.158771324027147,0.275,0.));
#17932=CARTESIAN_POINT('Origin',(0.317542648054294,0.,0.));
#17933=CARTESIAN_POINT('',(0.317542648054294,0.,0.));
#17934=CARTESIAN_POINT('',(0.317542648054294,0.,0.));
#17935=CARTESIAN_POINT('',(0.317542648054294,0.,0.));
#17936=CARTESIAN_POINT('Origin',(0.158771324027147,-0.275,0.));
#17937=CARTESIAN_POINT('',(0.158771324027147,-0.275,0.));
#17938=CARTESIAN_POINT('Origin',(0.,0.,0.));
#18565=UNCERTAINTY_MEASURE_WITH_UNIT(LENGTH_MEASURE(0.001),#18581,
'DISTANCE_ACCURACY_VALUE',
'Maximum model space distance between geometric entities at asserted c
onnectivities');
#18568=UNCERTAINTY_MEASURE_WITH_UNIT(LENGTH_MEASURE(0.001),#18581,
'DISTANCE_ACCURACY_VALUE',
'Maximum model space distance between geometric entities at asserted c
onnectivities');
#18577=(
GEOMETRIC_REPRESENTATION_CONTEXT(3)
GLOBAL_UNCERTAINTY_ASSIGNED_CONTEXT((#18565))
GLOBAL_UNIT_ASSIGNED_CONTEXT((#18581,#18583,#18584))
REPRESENTATION_CONTEXT('','3D')
);
#18580=(
GEOMETRIC_REPRESENTATION_CONTEXT(3)
GLOBAL_UNCERTAINTY_ASSIGNED_CONTEXT((#18568))
GLOBAL_UNIT_ASSIGNED_CONTEXT((#18581,#18583,#18584))
REPRESENTATION_CONTEXT('','3D')
);
#18581=(
LENGTH_UNIT()
NAMED_UNIT(*)
SI_UNIT(.CENTI.,.METRE.)
);
#18583=(
NAMED_UNIT(*)
PLANE_ANGLE_UNIT()
SI_UNIT($,.RADIAN.)
);
#18584=(
NAMED_UNIT(*)
SI_UNIT($,.STERADIAN.)
SOLID_ANGLE_UNIT()
);
#18593=SHAPE_DEFINITION_REPRESENTATION(#18604,#18631);
#18604=PRODUCT_DEFINITION_SHAPE('',$,#18643);
#18631=SHAPE_REPRESENTATION('',(#7030),#18577);
#18634=PRODUCT_DEFINITION_CONTEXT('part definition',#18669,'design');
#18643=PRODUCT_DEFINITION('2026-11-10-05-09-36-734','Hex nut M3',#18654,
#18634);
#18654=PRODUCT_DEFINITION_FORMATION('',$,#18679);
#18669=APPLICATION_CONTEXT(
'Core Data for Automotive Mechanical Design Process');
#18670=PRODUCT_CONTEXT('part definition',#18669,'mechanical');
#18679=PRODUCT('2026-11-10-05-09-36-734','Hex nut M3',$,(#18670));
#18687=PRESENTATION_STYLE_ASSIGNMENT((#18695));
#18695=SURFACE_STYLE_USAGE(.BOTH.,#18703);
#18703=SURFACE_SIDE_STYLE('',(#18711));
#18711=SURFACE_STYLE_FILL_AREA(#18719);
#18719=FILL_AREA_STYLE('Fastener gray',(#18727));
#18727=FILL_AREA_STYLE_COLOUR('Fastener gray',#18735);
#18735=COLOUR_RGB('Fastener gray',0.607843137254902,0.643137254901961,0.698039215686274);
ENDSEC;
END-ISO-10303-21;
